ISO-10303-21;
HEADER;
/* Generated by software containing ST-Developer
 * from STEP Tools, Inc. (www.steptools.com) 
 */

FILE_DESCRIPTION(
/* description */ ('STEP AP214'),
/* implementation_level */ '2;1');

FILE_NAME(
/* name */ 'TPS - Throttle Position Sensor.step',
/* time_stamp */ '2026-10-07T12:18:07-07:00',
/* author */ (''),
/* organization */ (''),
/* preprocessor_version */ 'ST-DEVELOPER v20.2',
/* originating_system */ 'Autodesk Translation Framework v15.15.0.0',
/* authorisation */ '');

FILE_SCHEMA (('AUTOMOTIVE_DESIGN { 1 0 10303 214 3 1 1 }'));
ENDSEC;

DATA;
#10=MECHANICAL_DESIGN_GEOMETRIC_PRESENTATION_REPRESENTATION('',(#125),#62974);
#101=SHAPE_REPRESENTATION_RELATIONSHIP('SRR','None',#63024,#113);
#113=ADVANCED_BREP_SHAPE_REPRESENTATION('',(#137),#62965);
#125=STYLED_ITEM('',(#63090),#137);
#137=MANIFOLD_SOLID_BREP('Body1',#15195);
#217=FACE_BOUND('',#4826,.T.);
#218=FACE_BOUND('',#4828,.T.);
#219=FACE_BOUND('',#4832,.T.);
#220=FACE_BOUND('',#4865,.T.);
#221=FACE_BOUND('',#4898,.T.);
#222=FACE_BOUND('',#4899,.T.);
#223=FACE_BOUND('',#4900,.T.);
#431=PLANE('',#15698);
#432=PLANE('',#15699);
#433=PLANE('',#15700);
#434=PLANE('',#15701);
#435=PLANE('',#15702);
#436=PLANE('',#15703);
#437=PLANE('',#15704);
#438=PLANE('',#15705);
#439=PLANE('',#15706);
#440=PLANE('',#15707);
#441=PLANE('',#15708);
#442=PLANE('',#15709);
#443=PLANE('',#15710);
#444=PLANE('',#15713);
#445=PLANE('',#15716);
#446=PLANE('',#15717);
#447=PLANE('',#15718);
#448=PLANE('',#15719);
#449=PLANE('',#15720);
#450=PLANE('',#15721);
#451=PLANE('',#15722);
#452=PLANE('',#15723);
#453=PLANE('',#15724);
#454=PLANE('',#15725);
#455=PLANE('',#15726);
#456=PLANE('',#15730);
#457=PLANE('',#15731);
#458=PLANE('',#15738);
#459=PLANE('',#15739);
#460=PLANE('',#15740);
#461=PLANE('',#15744);
#462=PLANE('',#15745);
#463=PLANE('',#15746);
#464=PLANE('',#15747);
#465=PLANE('',#15748);
#466=PLANE('',#15749);
#467=PLANE('',#15753);
#468=PLANE('',#15760);
#469=PLANE('',#15767);
#470=PLANE('',#15774);
#471=PLANE('',#15775);
#472=PLANE('',#15776);
#473=PLANE('',#15777);
#474=PLANE('',#15778);
#475=PLANE('',#15780);
#476=PLANE('',#15781);
#477=PLANE('',#15782);
#478=PLANE('',#15783);
#479=PLANE('',#15784);
#480=PLANE('',#15785);
#481=PLANE('',#15786);
#482=PLANE('',#15787);
#483=PLANE('',#15788);
#484=PLANE('',#15789);
#485=PLANE('',#15790);
#486=PLANE('',#15791);
#487=PLANE('',#15792);
#488=PLANE('',#15793);
#489=PLANE('',#15794);
#490=PLANE('',#15795);
#491=PLANE('',#15796);
#492=PLANE('',#15797);
#493=PLANE('',#15798);
#494=PLANE('',#15804);
#495=PLANE('',#15805);
#496=PLANE('',#15806);
#497=PLANE('',#15807);
#498=PLANE('',#15808);
#499=PLANE('',#15809);
#500=PLANE('',#15816);
#501=PLANE('',#15817);
#502=PLANE('',#15819);
#503=PLANE('',#15820);
#504=PLANE('',#15821);
#505=PLANE('',#15822);
#506=PLANE('',#15823);
#507=PLANE('',#15827);
#508=PLANE('',#15828);
#509=PLANE('',#15829);
#510=PLANE('',#15830);
#511=PLANE('',#15831);
#512=PLANE('',#15832);
#513=PLANE('',#15835);
#514=PLANE('',#15838);
#515=PLANE('',#15843);
#516=PLANE('',#15844);
#517=PLANE('',#15845);
#518=PLANE('',#15846);
#519=PLANE('',#15847);
#520=PLANE('',#15848);
#521=PLANE('',#15849);
#522=PLANE('',#15850);
#523=PLANE('',#15851);
#524=PLANE('',#15852);
#525=PLANE('',#15853);
#526=PLANE('',#15854);
#527=PLANE('',#15855);
#528=PLANE('',#15856);
#529=PLANE('',#15857);
#751=ELLIPSE('',#15714,2.022122546197,0.800000000000197);
#752=ELLIPSE('',#15715,5.05530636499052,1.99999999968039);
#753=ELLIPSE('',#15815,5.0553063659433,2.00000000029026);
#754=ELLIPSE('',#15825,2.02212254619594,0.799999999999696);
#1037=CONICAL_SURFACE('',#15727,2.5,0.174532925199433);
#1038=CONICAL_SURFACE('',#15732,2.5,0.174532925199434);
#1039=CONICAL_SURFACE('',#15735,2.5,0.174532925199435);
#1040=CONICAL_SURFACE('',#15741,2.5,0.174532925199433);
#1355=LINE('',#34485,#2548);
#1356=LINE('',#34488,#2549);
#1357=LINE('',#34493,#2550);
#1358=LINE('',#34500,#2551);
#1359=LINE('',#34503,#2552);
#1360=LINE('',#34509,#2553);
#1361=LINE('',#34512,#2554);
#1362=LINE('',#34518,#2555);
#1363=LINE('',#34523,#2556);
#1364=LINE('',#34527,#2557);
#1365=LINE('',#34529,#2558);
#1366=LINE('',#34531,#2559);
#1367=LINE('',#34532,#2560);
#1368=LINE('',#34535,#2561);
#1369=LINE('',#34537,#2562);
#1370=LINE('',#34538,#2563);
#1371=LINE('',#34541,#2564);
#1372=LINE('',#34543,#2565);
#1373=LINE('',#34544,#2566);
#1374=LINE('',#34548,#2567);
#1375=LINE('',#34550,#2568);
#1376=LINE('',#34552,#2569);
#1377=LINE('',#34553,#2570);
#1378=LINE('',#34557,#2571);
#1379=LINE('',#34558,#2572);
#1380=LINE('',#34559,#2573);
#1381=LINE('',#34563,#2574);
#1382=LINE('',#34564,#2575);
#1383=LINE('',#34565,#2576);
#1384=LINE('',#34569,#2577);
#1385=LINE('',#34571,#2578);
#1386=LINE('',#34573,#2579);
#1387=LINE('',#34574,#2580);
#1388=LINE('',#34578,#2581);
#1389=LINE('',#34580,#2582);
#1390=LINE('',#34582,#2583);
#1391=LINE('',#34583,#2584);
#1392=LINE('',#34585,#2585);
#1393=LINE('',#34587,#2586);
#1394=LINE('',#34589,#2587);
#1395=LINE('',#34590,#2588);
#1396=LINE('',#34592,#2589);
#1397=LINE('',#34594,#2590);
#1398=LINE('',#34596,#2591);
#1399=LINE('',#34598,#2592);
#1400=LINE('',#34600,#2593);
#1401=LINE('',#34601,#2594);
#1402=LINE('',#34605,#2595);
#1403=LINE('',#34606,#2596);
#1404=LINE('',#34607,#2597);
#1405=LINE('',#34611,#2598);
#1406=LINE('',#34612,#2599);
#1407=LINE('',#34613,#2600);
#1408=LINE('',#34619,#2601);
#1409=LINE('',#34620,#2602);
#1410=LINE('',#34622,#2603);
#1411=LINE('',#34624,#2604);
#1412=LINE('',#34627,#2605);
#1413=LINE('',#34631,#2606);
#1414=LINE('',#34633,#2607);
#1415=LINE('',#34635,#2608);
#1416=LINE('',#34641,#2609);
#1417=LINE('',#34643,#2610);
#1418=LINE('',#34645,#2611);
#1419=LINE('',#34647,#2612);
#1420=LINE('',#34649,#2613);
#1421=LINE('',#34650,#2614);
#1422=LINE('',#34654,#2615);
#1423=LINE('',#34656,#2616);
#1424=LINE('',#34658,#2617);
#1425=LINE('',#34660,#2618);
#1426=LINE('',#34662,#2619);
#1427=LINE('',#34663,#2620);
#1428=LINE('',#34666,#2621);
#1429=LINE('',#34668,#2622);
#1430=LINE('',#34669,#2623);
#1431=LINE('',#34673,#2624);
#1432=LINE('',#34675,#2625);
#1433=LINE('',#34677,#2626);
#1434=LINE('',#34678,#2627);
#1435=LINE('',#34682,#2628);
#1436=LINE('',#34684,#2629);
#1437=LINE('',#34686,#2630);
#1438=LINE('',#34687,#2631);
#1439=LINE('',#34688,#2632);
#1440=LINE('',#34691,#2633);
#1441=LINE('',#34692,#2634);
#1442=LINE('',#34695,#2635);
#1443=LINE('',#34697,#2636);
#1444=LINE('',#34698,#2637);
#1445=LINE('',#34700,#2638);
#1446=LINE('',#34703,#2639);
#1447=LINE('',#34704,#2640);
#1448=LINE('',#34708,#2641);
#1449=LINE('',#34709,#2642);
#1450=LINE('',#34710,#2643);
#1451=LINE('',#34712,#2644);
#1452=LINE('',#34716,#2645);
#1453=LINE('',#34720,#2646);
#1454=LINE('',#34724,#2647);
#1455=LINE('',#34726,#2648);
#1456=LINE('',#34727,#2649);
#1457=LINE('',#34730,#2650);
#1458=LINE('',#34732,#2651);
#1459=LINE('',#34733,#2652);
#1460=LINE('',#34738,#2653);
#1461=LINE('',#34744,#2654);
#1462=LINE('',#34748,#2655);
#1463=LINE('',#34750,#2656);
#1464=LINE('',#34751,#2657);
#1465=LINE('',#34754,#2658);
#1466=LINE('',#34756,#2659);
#1467=LINE('',#34757,#2660);
#1468=LINE('',#34760,#2661);
#1469=LINE('',#34761,#2662);
#1470=LINE('',#34766,#2663);
#1471=LINE('',#34768,#2664);
#1472=LINE('',#34769,#2665);
#1473=LINE('',#34774,#2666);
#1474=LINE('',#34776,#2667);
#1475=LINE('',#34777,#2668);
#1476=LINE('',#34778,#2669);
#1477=LINE('',#34779,#2670);
#1478=LINE('',#34782,#2671);
#1479=LINE('',#34784,#2672);
#1480=LINE('',#34785,#2673);
#1481=LINE('',#34791,#2674);
#1482=LINE('',#34794,#2675);
#1483=LINE('',#34796,#2676);
#1484=LINE('',#34798,#2677);
#1485=LINE('',#34799,#2678);
#1486=LINE('',#34805,#2679);
#1487=LINE('',#34810,#2680);
#1488=LINE('',#34813,#2681);
#1489=LINE('',#34814,#2682);
#1490=LINE('',#34819,#2683);
#1491=LINE('',#34826,#2684);
#1492=LINE('',#34829,#2685);
#1493=LINE('',#34831,#2686);
#1494=LINE('',#34832,#2687);
#1495=LINE('',#34841,#2688);
#1496=LINE('',#34843,#2689);
#1497=LINE('',#34845,#2690);
#1498=LINE('',#34847,#2691);
#1499=LINE('',#34852,#2692);
#1500=LINE('',#34856,#2693);
#1501=LINE('',#34858,#2694);
#1502=LINE('',#34859,#2695);
#1503=LINE('',#34861,#2696);
#1504=LINE('',#34865,#2697);
#1505=LINE('',#34867,#2698);
#1506=LINE('',#34869,#2699);
#1507=LINE('',#34870,#2700);
#1508=LINE('',#34872,#2701);
#1509=LINE('',#34873,#2702);
#1510=LINE('',#34878,#2703);
#1511=LINE('',#34880,#2704);
#1512=LINE('',#34882,#2705);
#1513=LINE('',#34883,#2706);
#1514=LINE('',#34884,#2707);
#1515=LINE('',#34888,#2708);
#1516=LINE('',#34889,#2709);
#1517=LINE('',#34890,#2710);
#1518=LINE('',#34892,#2711);
#1519=LINE('',#34893,#2712);
#1520=LINE('',#34896,#2713);
#1521=LINE('',#34898,#2714);
#1522=LINE('',#34900,#2715);
#1523=LINE('',#34902,#2716);
#1524=LINE('',#34904,#2717);
#1525=LINE('',#34905,#2718);
#1526=LINE('',#34907,#2719);
#1527=LINE('',#34908,#2720);
#1528=LINE('',#34911,#2721);
#1529=LINE('',#34913,#2722);
#1530=LINE('',#34914,#2723);
#1531=LINE('',#34917,#2724);
#1532=LINE('',#34919,#2725);
#1533=LINE('',#34920,#2726);
#1534=LINE('',#34922,#2727);
#1535=LINE('',#34924,#2728);
#1536=LINE('',#34926,#2729);
#1537=LINE('',#34929,#2730);
#1538=LINE('',#34931,#2731);
#1539=LINE('',#34932,#2732);
#1540=LINE('',#34934,#2733);
#1541=LINE('',#34936,#2734);
#1542=LINE('',#34939,#2735);
#1543=LINE('',#34940,#2736);
#1544=LINE('',#34943,#2737);
#1545=LINE('',#34945,#2738);
#1546=LINE('',#34947,#2739);
#1547=LINE('',#34948,#2740);
#1548=LINE('',#34951,#2741);
#1549=LINE('',#34953,#2742);
#1550=LINE('',#34954,#2743);
#1551=LINE('',#34956,#2744);
#1552=LINE('',#34958,#2745);
#1553=LINE('',#34960,#2746);
#1554=LINE('',#34961,#2747);
#1555=LINE('',#34964,#2748);
#1556=LINE('',#34966,#2749);
#1557=LINE('',#34967,#2750);
#1558=LINE('',#34974,#2751);
#1559=LINE('',#34977,#2752);
#1560=LINE('',#34978,#2753);
#1561=LINE('',#34981,#2754);
#1562=LINE('',#34983,#2755);
#1563=LINE('',#34984,#2756);
#1564=LINE('',#34987,#2757);
#1565=LINE('',#34989,#2758);
#1566=LINE('',#34990,#2759);
#1567=LINE('',#34992,#2760);
#1568=LINE('',#34994,#2761);
#1569=LINE('',#34995,#2762);
#1570=LINE('',#34998,#2763);
#1571=LINE('',#34999,#2764);
#1572=LINE('',#35000,#2765);
#1573=LINE('',#35003,#2766);
#1574=LINE('',#35005,#2767);
#1575=LINE('',#35008,#2768);
#1576=LINE('',#35010,#2769);
#1577=LINE('',#35014,#2770);
#1578=LINE('',#35019,#2771);
#1579=LINE('',#35020,#2772);
#1580=LINE('',#35023,#2773);
#1581=LINE('',#35025,#2774);
#1582=LINE('',#35028,#2775);
#1583=LINE('',#35031,#2776);
#1584=LINE('',#35032,#2777);
#1585=LINE('',#35035,#2778);
#1586=LINE('',#35037,#2779);
#1587=LINE('',#35039,#2780);
#1588=LINE('',#35040,#2781);
#1589=LINE('',#35044,#2782);
#1590=LINE('',#35047,#2783);
#1591=LINE('',#35050,#2784);
#1592=LINE('',#35051,#2785);
#1593=LINE('',#35054,#2786);
#1594=LINE('',#35055,#2787);
#1595=LINE('',#35058,#2788);
#1596=LINE('',#35060,#2789);
#1597=LINE('',#35061,#2790);
#1598=LINE('',#35063,#2791);
#1599=LINE('',#35067,#2792);
#1600=LINE('',#35069,#2793);
#1601=LINE('',#35070,#2794);
#1602=LINE('',#35073,#2795);
#1603=LINE('',#35077,#2796);
#1604=LINE('',#35078,#2797);
#1605=LINE('',#35081,#2798);
#1606=LINE('',#35085,#2799);
#1607=LINE('',#35086,#2800);
#1608=LINE('',#35089,#2801);
#1609=LINE('',#35093,#2802);
#1610=LINE('',#35098,#2803);
#1611=LINE('',#35099,#2804);
#1612=LINE('',#35100,#2805);
#1613=LINE('',#35102,#2806);
#1614=LINE('',#35103,#2807);
#1615=LINE('',#35108,#2808);
#1616=LINE('',#35110,#2809);
#1617=LINE('',#35112,#2810);
#1618=LINE('',#35113,#2811);
#1619=LINE('',#35117,#2812);
#1620=LINE('',#35119,#2813);
#1621=LINE('',#35121,#2814);
#1622=LINE('',#35122,#2815);
#1623=LINE('',#35126,#2816);
#1624=LINE('',#35127,#2817);
#1625=LINE('',#35128,#2818);
#1626=LINE('',#35129,#2819);
#1627=LINE('',#35132,#2820);
#1628=LINE('',#35133,#2821);
#1629=LINE('',#35136,#2822);
#1630=LINE('',#35137,#2823);
#1631=LINE('',#35139,#2824);
#1632=LINE('',#35140,#2825);
#1633=LINE('',#35143,#2826);
#1634=LINE('',#35144,#2827);
#1635=LINE('',#35146,#2828);
#2548=VECTOR('',#17948,1000.);
#2549=VECTOR('',#17951,1000.);
#2550=VECTOR('',#17956,2.067);
#2551=VECTOR('',#17963,1000.);
#2552=VECTOR('',#17966,1000.);
#2553=VECTOR('',#17971,1000.);
#2554=VECTOR('',#17974,1000.);
#2555=VECTOR('',#17979,1000.);
#2556=VECTOR('',#17984,1000.);
#2557=VECTOR('',#17987,1000.);
#2558=VECTOR('',#17988,1000.);
#2559=VECTOR('',#17989,1000.);
#2560=VECTOR('',#17990,1000.);
#2561=VECTOR('',#17993,1000.);
#2562=VECTOR('',#17994,1000.);
#2563=VECTOR('',#17995,1000.);
#2564=VECTOR('',#17998,1000.);
#2565=VECTOR('',#17999,1000.);
#2566=VECTOR('',#18000,1000.);
#2567=VECTOR('',#18003,1000.);
#2568=VECTOR('',#18004,1000.);
#2569=VECTOR('',#18005,1000.);
#2570=VECTOR('',#18006,1000.);
#2571=VECTOR('',#18009,1000.);
#2572=VECTOR('',#18010,1000.);
#2573=VECTOR('',#18011,1000.);
#2574=VECTOR('',#18014,1000.);
#2575=VECTOR('',#18015,1000.);
#2576=VECTOR('',#18016,1000.);
#2577=VECTOR('',#18019,1000.);
#2578=VECTOR('',#18020,1000.);
#2579=VECTOR('',#18021,1000.);
#2580=VECTOR('',#18022,1000.);
#2581=VECTOR('',#18025,1000.);
#2582=VECTOR('',#18026,1000.);
#2583=VECTOR('',#18027,1000.);
#2584=VECTOR('',#18028,1000.);
#2585=VECTOR('',#18031,1000.);
#2586=VECTOR('',#18032,1000.);
#2587=VECTOR('',#18033,1000.);
#2588=VECTOR('',#18034,1000.);
#2589=VECTOR('',#18037,1000.);
#2590=VECTOR('',#18038,1000.);
#2591=VECTOR('',#18039,1000.);
#2592=VECTOR('',#18040,1000.);
#2593=VECTOR('',#18041,1000.);
#2594=VECTOR('',#18042,1000.);
#2595=VECTOR('',#18045,1000.);
#2596=VECTOR('',#18046,1000.);
#2597=VECTOR('',#18047,1000.);
#2598=VECTOR('',#18050,1000.);
#2599=VECTOR('',#18051,1000.);
#2600=VECTOR('',#18052,1000.);
#2601=VECTOR('',#18057,1000.);
#2602=VECTOR('',#18058,1000.);
#2603=VECTOR('',#18059,1000.);
#2604=VECTOR('',#18060,1000.);
#2605=VECTOR('',#18063,1000.);
#2606=VECTOR('',#18066,1000.);
#2607=VECTOR('',#18067,1000.);
#2608=VECTOR('',#18068,1000.);
#2609=VECTOR('',#18075,1000.);
#2610=VECTOR('',#18076,1000.);
#2611=VECTOR('',#18077,1000.);
#2612=VECTOR('',#18078,1000.);
#2613=VECTOR('',#18079,1000.);
#2614=VECTOR('',#18080,1000.);
#2615=VECTOR('',#18083,1000.);
#2616=VECTOR('',#18084,1000.);
#2617=VECTOR('',#18085,1000.);
#2618=VECTOR('',#18086,1000.);
#2619=VECTOR('',#18087,1000.);
#2620=VECTOR('',#18088,1000.);
#2621=VECTOR('',#18091,1000.);
#2622=VECTOR('',#18092,1000.);
#2623=VECTOR('',#18093,1000.);
#2624=VECTOR('',#18096,1000.);
#2625=VECTOR('',#18097,1000.);
#2626=VECTOR('',#18098,1000.);
#2627=VECTOR('',#18099,1000.);
#2628=VECTOR('',#18102,1000.);
#2629=VECTOR('',#18103,1000.);
#2630=VECTOR('',#18104,1000.);
#2631=VECTOR('',#18105,1000.);
#2632=VECTOR('',#18106,1000.);
#2633=VECTOR('',#18109,1000.);
#2634=VECTOR('',#18110,1000.);
#2635=VECTOR('',#18113,1000.);
#2636=VECTOR('',#18114,1000.);
#2637=VECTOR('',#18115,1000.);
#2638=VECTOR('',#18118,1000.);
#2639=VECTOR('',#18121,1000.);
#2640=VECTOR('',#18122,1000.);
#2641=VECTOR('',#18125,1000.);
#2642=VECTOR('',#18126,1000.);
#2643=VECTOR('',#18127,1000.);
#2644=VECTOR('',#18130,1000.);
#2645=VECTOR('',#18133,1000.);
#2646=VECTOR('',#18136,1000.);
#2647=VECTOR('',#18141,1000.);
#2648=VECTOR('',#18142,1000.);
#2649=VECTOR('',#18143,1000.);
#2650=VECTOR('',#18146,1000.);
#2651=VECTOR('',#18147,1000.);
#2652=VECTOR('',#18148,1000.);
#2653=VECTOR('',#18153,1000.);
#2654=VECTOR('',#18160,1000.);
#2655=VECTOR('',#18165,1000.);
#2656=VECTOR('',#18166,1000.);
#2657=VECTOR('',#18167,1000.);
#2658=VECTOR('',#18170,1000.);
#2659=VECTOR('',#18171,1000.);
#2660=VECTOR('',#18172,1000.);
#2661=VECTOR('',#18175,1000.);
#2662=VECTOR('',#18176,1000.);
#2663=VECTOR('',#18185,1000.);
#2664=VECTOR('',#18188,1000.);
#2665=VECTOR('',#18189,1000.);
#2666=VECTOR('',#18196,1000.);
#2667=VECTOR('',#18197,1000.);
#2668=VECTOR('',#18198,1000.);
#2669=VECTOR('',#18199,1000.);
#2670=VECTOR('',#18200,1000.);
#2671=VECTOR('',#18203,1000.);
#2672=VECTOR('',#18204,1000.);
#2673=VECTOR('',#18205,1000.);
#2674=VECTOR('',#18212,1000.);
#2675=VECTOR('',#18215,1000.);
#2676=VECTOR('',#18216,1000.);
#2677=VECTOR('',#18217,1000.);
#2678=VECTOR('',#18218,1000.);
#2679=VECTOR('',#18225,1000.);
#2680=VECTOR('',#18230,1000.);
#2681=VECTOR('',#18235,1000.);
#2682=VECTOR('',#18236,1000.);
#2683=VECTOR('',#18241,1000.);
#2684=VECTOR('',#18250,1000.);
#2685=VECTOR('',#18253,1000.);
#2686=VECTOR('',#18254,1000.);
#2687=VECTOR('',#18255,1000.);
#2688=VECTOR('',#18268,1000.);
#2689=VECTOR('',#18271,1000.);
#2690=VECTOR('',#18274,1000.);
#2691=VECTOR('',#18277,1000.);
#2692=VECTOR('',#18282,1000.);
#2693=VECTOR('',#18285,1000.);
#2694=VECTOR('',#18286,1000.);
#2695=VECTOR('',#18287,1000.);
#2696=VECTOR('',#18290,1000.);
#2697=VECTOR('',#18293,1000.);
#2698=VECTOR('',#18294,1000.);
#2699=VECTOR('',#18295,1000.);
#2700=VECTOR('',#18296,1000.);
#2701=VECTOR('',#18297,1000.);
#2702=VECTOR('',#18298,1000.);
#2703=VECTOR('',#18303,1000.);
#2704=VECTOR('',#18304,1000.);
#2705=VECTOR('',#18305,1000.);
#2706=VECTOR('',#18306,1000.);
#2707=VECTOR('',#18307,1000.);
#2708=VECTOR('',#18310,1000.);
#2709=VECTOR('',#18311,1000.);
#2710=VECTOR('',#18312,1000.);
#2711=VECTOR('',#18313,1000.);
#2712=VECTOR('',#18314,1000.);
#2713=VECTOR('',#18317,1000.);
#2714=VECTOR('',#18318,1000.);
#2715=VECTOR('',#18319,1000.);
#2716=VECTOR('',#18320,1000.);
#2717=VECTOR('',#18321,1000.);
#2718=VECTOR('',#18322,1000.);
#2719=VECTOR('',#18323,1000.);
#2720=VECTOR('',#18324,1000.);
#2721=VECTOR('',#18327,1000.);
#2722=VECTOR('',#18328,1000.);
#2723=VECTOR('',#18329,1000.);
#2724=VECTOR('',#18332,1000.);
#2725=VECTOR('',#18333,1000.);
#2726=VECTOR('',#18334,1000.);
#2727=VECTOR('',#18337,1000.);
#2728=VECTOR('',#18340,1000.);
#2729=VECTOR('',#18343,1000.);
#2730=VECTOR('',#18346,1000.);
#2731=VECTOR('',#18347,1000.);
#2732=VECTOR('',#18348,1000.);
#2733=VECTOR('',#18351,1000.);
#2734=VECTOR('',#18354,1000.);
#2735=VECTOR('',#18357,1000.);
#2736=VECTOR('',#18358,1000.);
#2737=VECTOR('',#18361,1000.);
#2738=VECTOR('',#18362,1000.);
#2739=VECTOR('',#18363,1000.);
#2740=VECTOR('',#18364,1000.);
#2741=VECTOR('',#18367,1000.);
#2742=VECTOR('',#18368,1000.);
#2743=VECTOR('',#18369,1000.);
#2744=VECTOR('',#18372,1000.);
#2745=VECTOR('',#18373,1000.);
#2746=VECTOR('',#18374,1000.);
#2747=VECTOR('',#18375,1000.);
#2748=VECTOR('',#18378,1000.);
#2749=VECTOR('',#18379,1000.);
#2750=VECTOR('',#18380,1000.);
#2751=VECTOR('',#18391,1000.);
#2752=VECTOR('',#18394,1000.);
#2753=VECTOR('',#18395,1000.);
#2754=VECTOR('',#18398,1000.);
#2755=VECTOR('',#18399,1000.);
#2756=VECTOR('',#18400,1000.);
#2757=VECTOR('',#18403,1000.);
#2758=VECTOR('',#18404,1000.);
#2759=VECTOR('',#18405,1000.);
#2760=VECTOR('',#18408,1000.);
#2761=VECTOR('',#18409,1000.);
#2762=VECTOR('',#18410,1000.);
#2763=VECTOR('',#18413,1000.);
#2764=VECTOR('',#18414,1000.);
#2765=VECTOR('',#18415,1000.);
#2766=VECTOR('',#18418,1000.);
#2767=VECTOR('',#18419,1000.);
#2768=VECTOR('',#18422,1000.);
#2769=VECTOR('',#18423,1000.);
#2770=VECTOR('',#18428,1000.);
#2771=VECTOR('',#18435,1000.);
#2772=VECTOR('',#18436,1000.);
#2773=VECTOR('',#18441,1000.);
#2774=VECTOR('',#18442,1000.);
#2775=VECTOR('',#18445,1000.);
#2776=VECTOR('',#18448,1000.);
#2777=VECTOR('',#18449,1000.);
#2778=VECTOR('',#18452,1000.);
#2779=VECTOR('',#18453,1000.);
#2780=VECTOR('',#18454,1000.);
#2781=VECTOR('',#18455,1000.);
#2782=VECTOR('',#18462,1000.);
#2783=VECTOR('',#18465,1000.);
#2784=VECTOR('',#18470,1000.);
#2785=VECTOR('',#18471,1000.);
#2786=VECTOR('',#18474,1000.);
#2787=VECTOR('',#18475,1000.);
#2788=VECTOR('',#18480,1000.);
#2789=VECTOR('',#18481,1000.);
#2790=VECTOR('',#18482,1000.);
#2791=VECTOR('',#18485,1000.);
#2792=VECTOR('',#18490,1000.);
#2793=VECTOR('',#18491,1000.);
#2794=VECTOR('',#18492,1000.);
#2795=VECTOR('',#18495,1000.);
#2796=VECTOR('',#18500,1000.);
#2797=VECTOR('',#18501,1000.);
#2798=VECTOR('',#18504,1000.);
#2799=VECTOR('',#18509,1000.);
#2800=VECTOR('',#18510,1000.);
#2801=VECTOR('',#18513,1000.);
#2802=VECTOR('',#18518,1000.);
#2803=VECTOR('',#18527,1000.);
#2804=VECTOR('',#18528,1000.);
#2805=VECTOR('',#18529,1000.);
#2806=VECTOR('',#18532,1000.);
#2807=VECTOR('',#18533,1000.);
#2808=VECTOR('',#18538,1000.);
#2809=VECTOR('',#18539,1000.);
#2810=VECTOR('',#18540,1000.);
#2811=VECTOR('',#18541,1000.);
#2812=VECTOR('',#18544,1000.);
#2813=VECTOR('',#18545,1000.);
#2814=VECTOR('',#18546,1000.);
#2815=VECTOR('',#18547,1000.);
#2816=VECTOR('',#18550,1000.);
#2817=VECTOR('',#18551,1000.);
#2818=VECTOR('',#18552,1000.);
#2819=VECTOR('',#18553,1000.);
#2820=VECTOR('',#18556,1000.);
#2821=VECTOR('',#18557,1000.);
#2822=VECTOR('',#18560,1000.);
#2823=VECTOR('',#18561,1000.);
#2824=VECTOR('',#18564,1000.);
#2825=VECTOR('',#18565,1000.);
#2826=VECTOR('',#18568,1000.);
#2827=VECTOR('',#18569,1000.);
#2828=VECTOR('',#18572,1000.);
#3464=CYLINDRICAL_SURFACE('',#15680,9.6875);
#3465=CYLINDRICAL_SURFACE('',#15685,2.067);
#3466=CYLINDRICAL_SURFACE('',#15688,5.);
#3467=CYLINDRICAL_SURFACE('',#15691,9.);
#3468=CYLINDRICAL_SURFACE('',#15694,9.);
#3469=CYLINDRICAL_SURFACE('',#15750,9.);
#3470=CYLINDRICAL_SURFACE('',#15754,9.);
#3471=CYLINDRICAL_SURFACE('',#15757,9.);
#3472=CYLINDRICAL_SURFACE('',#15761,0.5);
#3473=CYLINDRICAL_SURFACE('',#15764,0.5);
#3474=CYLINDRICAL_SURFACE('',#15768,0.5);
#3475=CYLINDRICAL_SURFACE('',#15771,0.5);
#3476=CYLINDRICAL_SURFACE('',#15799,3.5);
#3477=CYLINDRICAL_SURFACE('',#15802,3.5);
#3478=CYLINDRICAL_SURFACE('',#15812,2.);
#3479=CYLINDRICAL_SURFACE('',#15814,2.);
#3480=CYLINDRICAL_SURFACE('',#15824,0.799999999999998);
#3481=CYLINDRICAL_SURFACE('',#15826,0.799999999999998);
#3482=CYLINDRICAL_SURFACE('',#15833,2.5);
#3483=CYLINDRICAL_SURFACE('',#15836,2.5);
#3484=CYLINDRICAL_SURFACE('',#15839,2.5);
#3485=CYLINDRICAL_SURFACE('',#15841,2.5);
#3879=FACE_OUTER_BOUND('',#4769,.T.);
#3880=FACE_OUTER_BOUND('',#4770,.T.);
#3881=FACE_OUTER_BOUND('',#4771,.T.);
#3882=FACE_OUTER_BOUND('',#4772,.T.);
#3883=FACE_OUTER_BOUND('',#4773,.T.);
#3884=FACE_OUTER_BOUND('',#4774,.T.);
#3885=FACE_OUTER_BOUND('',#4775,.T.);
#3886=FACE_OUTER_BOUND('',#4776,.T.);
#3887=FACE_OUTER_BOUND('',#4777,.T.);
#3888=FACE_OUTER_BOUND('',#4778,.T.);
#3889=FACE_OUTER_BOUND('',#4779,.T.);
#3890=FACE_OUTER_BOUND('',#4780,.T.);
#3891=FACE_OUTER_BOUND('',#4781,.T.);
#3892=FACE_OUTER_BOUND('',#4782,.T.);
#3893=FACE_OUTER_BOUND('',#4783,.T.);
#3894=FACE_OUTER_BOUND('',#4784,.T.);
#3895=FACE_OUTER_BOUND('',#4785,.T.);
#3896=FACE_OUTER_BOUND('',#4786,.T.);
#3897=FACE_OUTER_BOUND('',#4787,.T.);
#3898=FACE_OUTER_BOUND('',#4788,.T.);
#3899=FACE_OUTER_BOUND('',#4789,.T.);
#3900=FACE_OUTER_BOUND('',#4790,.T.);
#3901=FACE_OUTER_BOUND('',#4791,.T.);
#3902=FACE_OUTER_BOUND('',#4792,.T.);
#3903=FACE_OUTER_BOUND('',#4793,.T.);
#3904=FACE_OUTER_BOUND('',#4794,.T.);
#3905=FACE_OUTER_BOUND('',#4795,.T.);
#3906=FACE_OUTER_BOUND('',#4796,.T.);
#3907=FACE_OUTER_BOUND('',#4797,.T.);
#3908=FACE_OUTER_BOUND('',#4798,.T.);
#3909=FACE_OUTER_BOUND('',#4799,.T.);
#3910=FACE_OUTER_BOUND('',#4800,.T.);
#3911=FACE_OUTER_BOUND('',#4801,.T.);
#3912=FACE_OUTER_BOUND('',#4802,.T.);
#3913=FACE_OUTER_BOUND('',#4803,.T.);
#3914=FACE_OUTER_BOUND('',#4804,.T.);
#3915=FACE_OUTER_BOUND('',#4805,.T.);
#3916=FACE_OUTER_BOUND('',#4806,.T.);
#3917=FACE_OUTER_BOUND('',#4807,.T.);
#3918=FACE_OUTER_BOUND('',#4808,.T.);
#3919=FACE_OUTER_BOUND('',#4809,.T.);
#3920=FACE_OUTER_BOUND('',#4810,.T.);
#3921=FACE_OUTER_BOUND('',#4811,.T.);
#3922=FACE_OUTER_BOUND('',#4812,.T.);
#3923=FACE_OUTER_BOUND('',#4813,.T.);
#3924=FACE_OUTER_BOUND('',#4814,.T.);
#3925=FACE_OUTER_BOUND('',#4815,.T.);
#3926=FACE_OUTER_BOUND('',#4816,.T.);
#3927=FACE_OUTER_BOUND('',#4817,.T.);
#3928=FACE_OUTER_BOUND('',#4818,.T.);
#3929=FACE_OUTER_BOUND('',#4819,.T.);
#3930=FACE_OUTER_BOUND('',#4820,.T.);
#3931=FACE_OUTER_BOUND('',#4821,.T.);
#3932=FACE_OUTER_BOUND('',#4822,.T.);
#3933=FACE_OUTER_BOUND('',#4823,.T.);
#3934=FACE_OUTER_BOUND('',#4824,.T.);
#3935=FACE_OUTER_BOUND('',#4825,.T.);
#3936=FACE_OUTER_BOUND('',#4827,.T.);
#3937=FACE_OUTER_BOUND('',#4829,.T.);
#3938=FACE_OUTER_BOUND('',#4830,.T.);
#3939=FACE_OUTER_BOUND('',#4831,.T.);
#3940=FACE_OUTER_BOUND('',#4833,.T.);
#3941=FACE_OUTER_BOUND('',#4834,.T.);
#3942=FACE_OUTER_BOUND('',#4835,.T.);
#3943=FACE_OUTER_BOUND('',#4836,.T.);
#3944=FACE_OUTER_BOUND('',#4837,.T.);
#3945=FACE_OUTER_BOUND('',#4838,.T.);
#3946=FACE_OUTER_BOUND('',#4839,.T.);
#3947=FACE_OUTER_BOUND('',#4840,.T.);
#3948=FACE_OUTER_BOUND('',#4841,.T.);
#3949=FACE_OUTER_BOUND('',#4842,.T.);
#3950=FACE_OUTER_BOUND('',#4843,.T.);
#3951=FACE_OUTER_BOUND('',#4844,.T.);
#3952=FACE_OUTER_BOUND('',#4845,.T.);
#3953=FACE_OUTER_BOUND('',#4846,.T.);
#3954=FACE_OUTER_BOUND('',#4847,.T.);
#3955=FACE_OUTER_BOUND('',#4848,.T.);
#3956=FACE_OUTER_BOUND('',#4849,.T.);
#3957=FACE_OUTER_BOUND('',#4850,.T.);
#3958=FACE_OUTER_BOUND('',#4851,.T.);
#3959=FACE_OUTER_BOUND('',#4852,.T.);
#3960=FACE_OUTER_BOUND('',#4853,.T.);
#3961=FACE_OUTER_BOUND('',#4854,.T.);
#3962=FACE_OUTER_BOUND('',#4855,.T.);
#3963=FACE_OUTER_BOUND('',#4856,.T.);
#3964=FACE_OUTER_BOUND('',#4857,.T.);
#3965=FACE_OUTER_BOUND('',#4858,.T.);
#3966=FACE_OUTER_BOUND('',#4859,.T.);
#3967=FACE_OUTER_BOUND('',#4860,.T.);
#3968=FACE_OUTER_BOUND('',#4861,.T.);
#3969=FACE_OUTER_BOUND('',#4862,.T.);
#3970=FACE_OUTER_BOUND('',#4863,.T.);
#3971=FACE_OUTER_BOUND('',#4864,.T.);
#3972=FACE_OUTER_BOUND('',#4866,.T.);
#3973=FACE_OUTER_BOUND('',#4867,.T.);
#3974=FACE_OUTER_BOUND('',#4868,.T.);
#3975=FACE_OUTER_BOUND('',#4869,.T.);
#3976=FACE_OUTER_BOUND('',#4870,.T.);
#3977=FACE_OUTER_BOUND('',#4871,.T.);
#3978=FACE_OUTER_BOUND('',#4872,.T.);
#3979=FACE_OUTER_BOUND('',#4873,.T.);
#3980=FACE_OUTER_BOUND('',#4874,.T.);
#3981=FACE_OUTER_BOUND('',#4875,.T.);
#3982=FACE_OUTER_BOUND('',#4876,.T.);
#3983=FACE_OUTER_BOUND('',#4877,.T.);
#3984=FACE_OUTER_BOUND('',#4878,.T.);
#3985=FACE_OUTER_BOUND('',#4879,.T.);
#3986=FACE_OUTER_BOUND('',#4880,.T.);
#3987=FACE_OUTER_BOUND('',#4881,.T.);
#3988=FACE_OUTER_BOUND('',#4882,.T.);
#3989=FACE_OUTER_BOUND('',#4883,.T.);
#3990=FACE_OUTER_BOUND('',#4884,.T.);
#3991=FACE_OUTER_BOUND('',#4885,.T.);
#3992=FACE_OUTER_BOUND('',#4886,.T.);
#3993=FACE_OUTER_BOUND('',#4887,.T.);
#3994=FACE_OUTER_BOUND('',#4888,.T.);
#3995=FACE_OUTER_BOUND('',#4889,.T.);
#3996=FACE_OUTER_BOUND('',#4890,.T.);
#3997=FACE_OUTER_BOUND('',#4891,.T.);
#3998=FACE_OUTER_BOUND('',#4892,.T.);
#3999=FACE_OUTER_BOUND('',#4893,.T.);
#4000=FACE_OUTER_BOUND('',#4894,.T.);
#4001=FACE_OUTER_BOUND('',#4895,.T.);
#4002=FACE_OUTER_BOUND('',#4896,.T.);
#4003=FACE_OUTER_BOUND('',#4897,.T.);
#4769=EDGE_LOOP('',(#10743,#10744,#10745,#10746,#10747,#10748));
#4770=EDGE_LOOP('',(#10749,#10750,#10751,#10752));
#4771=EDGE_LOOP('',(#10753,#10754,#10755,#10756));
#4772=EDGE_LOOP('',(#10757,#10758,#10759,#10760));
#4773=EDGE_LOOP('',(#10761,#10762,#10763,#10764,#10765));
#4774=EDGE_LOOP('',(#10766,#10767,#10768,#10769));
#4775=EDGE_LOOP('',(#10770,#10771,#10772,#10773));
#4776=EDGE_LOOP('',(#10774,#10775,#10776,#10777));
#4777=EDGE_LOOP('',(#10778,#10779,#10780,#10781));
#4778=EDGE_LOOP('',(#10782,#10783,#10784,#10785));
#4779=EDGE_LOOP('',(#10786,#10787,#10788,#10789));
#4780=EDGE_LOOP('',(#10790,#10791,#10792,#10793));
#4781=EDGE_LOOP('',(#10794,#10795,#10796,#10797));
#4782=EDGE_LOOP('',(#10798,#10799,#10800,#10801,#10802,#10803));
#4783=EDGE_LOOP('',(#10804,#10805,#10806,#10807,#10808,#10809,#10810,#10811));
#4784=EDGE_LOOP('',(#10812,#10813,#10814,#10815));
#4785=EDGE_LOOP('',(#10816,#10817,#10818,#10819));
#4786=EDGE_LOOP('',(#10820,#10821,#10822,#10823,#10824,#10825,#10826,#10827));
#4787=EDGE_LOOP('',(#10828,#10829,#10830,#10831,#10832,#10833));
#4788=EDGE_LOOP('',(#10834,#10835,#10836,#10837,#10838,#10839));
#4789=EDGE_LOOP('',(#10840,#10841,#10842,#10843,#10844,#10845));
#4790=EDGE_LOOP('',(#10846,#10847,#10848,#10849));
#4791=EDGE_LOOP('',(#10850,#10851,#10852,#10853));
#4792=EDGE_LOOP('',(#10854,#10855,#10856,#10857,#10858,#10859));
#4793=EDGE_LOOP('',(#10860,#10861,#10862,#10863));
#4794=EDGE_LOOP('',(#10864,#10865,#10866,#10867));
#4795=EDGE_LOOP('',(#10868,#10869,#10870,#10871));
#4796=EDGE_LOOP('',(#10872,#10873,#10874,#10875));
#4797=EDGE_LOOP('',(#10876,#10877,#10878,#10879));
#4798=EDGE_LOOP('',(#10880,#10881,#10882,#10883));
#4799=EDGE_LOOP('',(#10884,#10885,#10886,#10887));
#4800=EDGE_LOOP('',(#10888,#10889,#10890,#10891));
#4801=EDGE_LOOP('',(#10892,#10893,#10894,#10895));
#4802=EDGE_LOOP('',(#10896,#10897,#10898,#10899));
#4803=EDGE_LOOP('',(#10900,#10901,#10902,#10903));
#4804=EDGE_LOOP('',(#10904,#10905,#10906,#10907));
#4805=EDGE_LOOP('',(#10908,#10909,#10910,#10911));
#4806=EDGE_LOOP('',(#10912,#10913,#10914,#10915));
#4807=EDGE_LOOP('',(#10916,#10917,#10918,#10919));
#4808=EDGE_LOOP('',(#10920,#10921,#10922,#10923));
#4809=EDGE_LOOP('',(#10924,#10925,#10926,#10927));
#4810=EDGE_LOOP('',(#10928,#10929,#10930,#10931));
#4811=EDGE_LOOP('',(#10932,#10933,#10934,#10935));
#4812=EDGE_LOOP('',(#10936,#10937,#10938,#10939,#10940,#10941));
#4813=EDGE_LOOP('',(#10942,#10943,#10944,#10945));
#4814=EDGE_LOOP('',(#10946,#10947,#10948,#10949));
#4815=EDGE_LOOP('',(#10950,#10951,#10952,#10953,#10954));
#4816=EDGE_LOOP('',(#10955,#10956,#10957,#10958));
#4817=EDGE_LOOP('',(#10959,#10960,#10961,#10962));
#4818=EDGE_LOOP('',(#10963,#10964,#10965,#10966));
#4819=EDGE_LOOP('',(#10967,#10968,#10969,#10970));
#4820=EDGE_LOOP('',(#10971,#10972,#10973,#10974));
#4821=EDGE_LOOP('',(#10975,#10976,#10977,#10978));
#4822=EDGE_LOOP('',(#10979,#10980,#10981,#10982));
#4823=EDGE_LOOP('',(#10983,#10984,#10985,#10986));
#4824=EDGE_LOOP('',(#10987,#10988,#10989,#10990));
#4825=EDGE_LOOP('',(#10991,#10992,#10993,#10994,#10995,#10996,#10997,#10998));
#4826=EDGE_LOOP('',(#10999,#11000,#11001,#11002,#11003,#11004,#11005,#11006));
#4827=EDGE_LOOP('',(#11007,#11008,#11009,#11010,#11011,#11012,#11013,#11014));
#4828=EDGE_LOOP('',(#11015));
#4829=EDGE_LOOP('',(#11016,#11017,#11018,#11019));
#4830=EDGE_LOOP('',(#11020,#11021,#11022,#11023,#11024));
#4831=EDGE_LOOP('',(#11025,#11026,#11027,#11028,#11029,#11030,#11031));
#4832=EDGE_LOOP('',(#11032));
#4833=EDGE_LOOP('',(#11033,#11034,#11035,#11036,#11037,#11038,#11039,#11040));
#4834=EDGE_LOOP('',(#11041,#11042));
#4835=EDGE_LOOP('',(#11043,#11044,#11045,#11046,#11047,#11048));
#4836=EDGE_LOOP('',(#11049,#11050,#11051,#11052,#11053,#11054,#11055,#11056));
#4837=EDGE_LOOP('',(#11057,#11058,#11059,#11060,#11061,#11062,#11063,#11064,
#11065,#11066,#11067,#11068,#11069,#11070,#11071));
#4838=EDGE_LOOP('',(#11072,#11073,#11074,#11075,#11076,#11077,#11078,#11079));
#4839=EDGE_LOOP('',(#11080,#11081,#11082,#11083));
#4840=EDGE_LOOP('',(#11084,#11085,#11086,#11087));
#4841=EDGE_LOOP('',(#11088,#11089,#11090,#11091));
#4842=EDGE_LOOP('',(#11092,#11093,#11094,#11095,#11096,#11097,#11098));
#4843=EDGE_LOOP('',(#11099,#11100,#11101,#11102));
#4844=EDGE_LOOP('',(#11103,#11104,#11105,#11106));
#4845=EDGE_LOOP('',(#11107,#11108,#11109,#11110));
#4846=EDGE_LOOP('',(#11111,#11112,#11113,#11114,#11115,#11116,#11117));
#4847=EDGE_LOOP('',(#11118,#11119,#11120,#11121,#11122));
#4848=EDGE_LOOP('',(#11123,#11124,#11125,#11126));
#4849=EDGE_LOOP('',(#11127,#11128,#11129,#11130,#11131));
#4850=EDGE_LOOP('',(#11132,#11133,#11134,#11135));
#4851=EDGE_LOOP('',(#11136,#11137,#11138,#11139));
#4852=EDGE_LOOP('',(#11140,#11141,#11142,#11143));
#4853=EDGE_LOOP('',(#11144,#11145,#11146,#11147));
#4854=EDGE_LOOP('',(#11148,#11149,#11150,#11151,#11152));
#4855=EDGE_LOOP('',(#11153,#11154,#11155,#11156));
#4856=EDGE_LOOP('',(#11157,#11158,#11159,#11160,#11161));
#4857=EDGE_LOOP('',(#11162,#11163,#11164,#11165,#11166,#11167));
#4858=EDGE_LOOP('',(#11168,#11169,#11170,#11171,#11172,#11173,#11174,#11175));
#4859=EDGE_LOOP('',(#11176,#11177,#11178,#11179,#11180));
#4860=EDGE_LOOP('',(#11181,#11182,#11183,#11184,#11185));
#4861=EDGE_LOOP('',(#11186,#11187,#11188,#11189));
#4862=EDGE_LOOP('',(#11190,#11191,#11192,#11193,#11194,#11195,#11196,#11197));
#4863=EDGE_LOOP('',(#11198,#11199,#11200,#11201,#11202,#11203));
#4864=EDGE_LOOP('',(#11204,#11205,#11206,#11207,#11208,#11209,#11210,#11211,
#11212,#11213,#11214,#11215,#11216,#11217,#11218,#11219,#11220,#11221));
#4865=EDGE_LOOP('',(#11222,#11223,#11224,#11225,#11226,#11227,#11228,#11229));
#4866=EDGE_LOOP('',(#11230,#11231,#11232,#11233,#11234,#11235,#11236,#11237));
#4867=EDGE_LOOP('',(#11238,#11239,#11240,#11241,#11242));
#4868=EDGE_LOOP('',(#11243,#11244,#11245,#11246,#11247));
#4869=EDGE_LOOP('',(#11248,#11249,#11250,#11251));
#4870=EDGE_LOOP('',(#11252,#11253,#11254,#11255));
#4871=EDGE_LOOP('',(#11256,#11257,#11258,#11259,#11260,#11261));
#4872=EDGE_LOOP('',(#11262,#11263,#11264,#11265));
#4873=EDGE_LOOP('',(#11266,#11267,#11268,#11269,#11270,#11271));
#4874=EDGE_LOOP('',(#11272,#11273,#11274,#11275));
#4875=EDGE_LOOP('',(#11276,#11277,#11278,#11279));
#4876=EDGE_LOOP('',(#11280,#11281,#11282,#11283));
#4877=EDGE_LOOP('',(#11284,#11285,#11286,#11287));
#4878=EDGE_LOOP('',(#11288,#11289,#11290,#11291));
#4879=EDGE_LOOP('',(#11292,#11293,#11294,#11295));
#4880=EDGE_LOOP('',(#11296,#11297,#11298,#11299));
#4881=EDGE_LOOP('',(#11300,#11301,#11302,#11303));
#4882=EDGE_LOOP('',(#11304,#11305,#11306,#11307));
#4883=EDGE_LOOP('',(#11308,#11309,#11310,#11311,#11312,#11313));
#4884=EDGE_LOOP('',(#11314,#11315,#11316,#11317,#11318));
#4885=EDGE_LOOP('',(#11319,#11320,#11321,#11322,#11323,#11324,#11325,#11326,
#11327,#11328,#11329,#11330));
#4886=EDGE_LOOP('',(#11331,#11332,#11333,#11334,#11335,#11336));
#4887=EDGE_LOOP('',(#11337,#11338,#11339,#11340));
#4888=EDGE_LOOP('',(#11341,#11342,#11343,#11344));
#4889=EDGE_LOOP('',(#11345,#11346,#11347,#11348));
#4890=EDGE_LOOP('',(#11349,#11350,#11351,#11352,#11353,#11354));
#4891=EDGE_LOOP('',(#11355,#11356,#11357,#11358));
#4892=EDGE_LOOP('',(#11359,#11360,#11361,#11362));
#4893=EDGE_LOOP('',(#11363,#11364,#11365,#11366,#11367,#11368));
#4894=EDGE_LOOP('',(#11369,#11370,#11371,#11372));
#4895=EDGE_LOOP('',(#11373,#11374,#11375,#11376,#11377,#11378));
#4896=EDGE_LOOP('',(#11379,#11380,#11381,#11382));
#4897=EDGE_LOOP('',(#11383,#11384,#11385,#11386,#11387,#11388,#11389,#11390,
#11391,#11392,#11393,#11394,#11395,#11396,#11397,#11398));
#4898=EDGE_LOOP('',(#11399,#11400,#11401,#11402));
#4899=EDGE_LOOP('',(#11403,#11404,#11405,#11406));
#4900=EDGE_LOOP('',(#11407,#11408,#11409,#11410));
#5647=CIRCLE('',#15681,9.6875);
#5648=CIRCLE('',#15682,9.6875);
#5649=CIRCLE('',#15683,9.6875);
#5650=CIRCLE('',#15684,9.6875);
#5651=CIRCLE('',#15686,2.067);
#5652=CIRCLE('',#15687,2.067);
#5653=CIRCLE('',#15689,5.);
#5654=CIRCLE('',#15690,5.);
#5655=CIRCLE('',#15692,9.);
#5656=CIRCLE('',#15693,9.);
#5657=CIRCLE('',#15695,9.);
#5658=CIRCLE('',#15696,9.);
#5659=CIRCLE('',#15697,9.);
#5660=CIRCLE('',#15711,2.);
#5661=CIRCLE('',#15712,2.);
#5662=CIRCLE('',#15728,2.8);
#5663=CIRCLE('',#15729,2.5);
#5664=CIRCLE('',#15733,2.8);
#5665=CIRCLE('',#15734,2.5);
#5666=CIRCLE('',#15736,2.5);
#5667=CIRCLE('',#15737,2.8);
#5668=CIRCLE('',#15742,2.8);
#5669=CIRCLE('',#15743,2.5);
#5670=CIRCLE('',#15751,8.99999999999999);
#5671=CIRCLE('',#15752,8.99999999999999);
#5672=CIRCLE('',#15755,9.);
#5673=CIRCLE('',#15756,9.);
#5674=CIRCLE('',#15758,8.99999999999999);
#5675=CIRCLE('',#15759,8.99999999999999);
#5676=CIRCLE('',#15762,0.500000000000001);
#5677=CIRCLE('',#15763,0.500000000000001);
#5678=CIRCLE('',#15765,0.500000000000001);
#5679=CIRCLE('',#15766,0.500000000000001);
#5680=CIRCLE('',#15769,0.500000000000001);
#5681=CIRCLE('',#15770,0.500000000000001);
#5682=CIRCLE('',#15772,0.500000000000001);
#5683=CIRCLE('',#15773,0.500000000000001);
#5684=CIRCLE('',#15779,3.5);
#5685=CIRCLE('',#15800,3.5);
#5686=CIRCLE('',#15801,3.5);
#5687=CIRCLE('',#15803,3.5);
#5688=CIRCLE('',#15810,2.);
#5689=CIRCLE('',#15811,0.799999999999998);
#5690=CIRCLE('',#15813,2.);
#5691=CIRCLE('',#15818,0.799999999999998);
#5692=CIRCLE('',#15834,2.5);
#5693=CIRCLE('',#15837,2.5);
#5694=CIRCLE('',#15840,2.5);
#5695=CIRCLE('',#15842,2.5);
#6510=VERTEX_POINT('',#34477);
#6511=VERTEX_POINT('',#34478);
#6512=VERTEX_POINT('',#34480);
#6513=VERTEX_POINT('',#34482);
#6514=VERTEX_POINT('',#34484);
#6515=VERTEX_POINT('',#34486);
#6516=VERTEX_POINT('',#34490);
#6517=VERTEX_POINT('',#34492);
#6518=VERTEX_POINT('',#34496);
#6519=VERTEX_POINT('',#34497);
#6520=VERTEX_POINT('',#34499);
#6521=VERTEX_POINT('',#34501);
#6522=VERTEX_POINT('',#34505);
#6523=VERTEX_POINT('',#34506);
#6524=VERTEX_POINT('',#34508);
#6525=VERTEX_POINT('',#34510);
#6526=VERTEX_POINT('',#34514);
#6527=VERTEX_POINT('',#34515);
#6528=VERTEX_POINT('',#34517);
#6529=VERTEX_POINT('',#34519);
#6530=VERTEX_POINT('',#34521);
#6531=VERTEX_POINT('',#34525);
#6532=VERTEX_POINT('',#34526);
#6533=VERTEX_POINT('',#34528);
#6534=VERTEX_POINT('',#34530);
#6535=VERTEX_POINT('',#34534);
#6536=VERTEX_POINT('',#34536);
#6537=VERTEX_POINT('',#34540);
#6538=VERTEX_POINT('',#34542);
#6539=VERTEX_POINT('',#34546);
#6540=VERTEX_POINT('',#34547);
#6541=VERTEX_POINT('',#34549);
#6542=VERTEX_POINT('',#34551);
#6543=VERTEX_POINT('',#34555);
#6544=VERTEX_POINT('',#34556);
#6545=VERTEX_POINT('',#34561);
#6546=VERTEX_POINT('',#34562);
#6547=VERTEX_POINT('',#34567);
#6548=VERTEX_POINT('',#34568);
#6549=VERTEX_POINT('',#34570);
#6550=VERTEX_POINT('',#34572);
#6551=VERTEX_POINT('',#34576);
#6552=VERTEX_POINT('',#34577);
#6553=VERTEX_POINT('',#34579);
#6554=VERTEX_POINT('',#34581);
#6555=VERTEX_POINT('',#34586);
#6556=VERTEX_POINT('',#34588);
#6557=VERTEX_POINT('',#34593);
#6558=VERTEX_POINT('',#34595);
#6559=VERTEX_POINT('',#34597);
#6560=VERTEX_POINT('',#34599);
#6561=VERTEX_POINT('',#34603);
#6562=VERTEX_POINT('',#34604);
#6563=VERTEX_POINT('',#34609);
#6564=VERTEX_POINT('',#34610);
#6565=VERTEX_POINT('',#34615);
#6566=VERTEX_POINT('',#34616);
#6567=VERTEX_POINT('',#34618);
#6568=VERTEX_POINT('',#34621);
#6569=VERTEX_POINT('',#34623);
#6570=VERTEX_POINT('',#34625);
#6571=VERTEX_POINT('',#34629);
#6572=VERTEX_POINT('',#34630);
#6573=VERTEX_POINT('',#34632);
#6574=VERTEX_POINT('',#34634);
#6575=VERTEX_POINT('',#34639);
#6576=VERTEX_POINT('',#34640);
#6577=VERTEX_POINT('',#34642);
#6578=VERTEX_POINT('',#34644);
#6579=VERTEX_POINT('',#34646);
#6580=VERTEX_POINT('',#34648);
#6581=VERTEX_POINT('',#34652);
#6582=VERTEX_POINT('',#34653);
#6583=VERTEX_POINT('',#34655);
#6584=VERTEX_POINT('',#34657);
#6585=VERTEX_POINT('',#34659);
#6586=VERTEX_POINT('',#34661);
#6587=VERTEX_POINT('',#34665);
#6588=VERTEX_POINT('',#34667);
#6589=VERTEX_POINT('',#34671);
#6590=VERTEX_POINT('',#34672);
#6591=VERTEX_POINT('',#34674);
#6592=VERTEX_POINT('',#34676);
#6593=VERTEX_POINT('',#34680);
#6594=VERTEX_POINT('',#34681);
#6595=VERTEX_POINT('',#34683);
#6596=VERTEX_POINT('',#34685);
#6597=VERTEX_POINT('',#34690);
#6598=VERTEX_POINT('',#34694);
#6599=VERTEX_POINT('',#34696);
#6600=VERTEX_POINT('',#34702);
#6601=VERTEX_POINT('',#34706);
#6602=VERTEX_POINT('',#34707);
#6603=VERTEX_POINT('',#34714);
#6604=VERTEX_POINT('',#34715);
#6605=VERTEX_POINT('',#34717);
#6606=VERTEX_POINT('',#34719);
#6607=VERTEX_POINT('',#34723);
#6608=VERTEX_POINT('',#34725);
#6609=VERTEX_POINT('',#34729);
#6610=VERTEX_POINT('',#34731);
#6611=VERTEX_POINT('',#34735);
#6612=VERTEX_POINT('',#34737);
#6613=VERTEX_POINT('',#34741);
#6614=VERTEX_POINT('',#34743);
#6615=VERTEX_POINT('',#34747);
#6616=VERTEX_POINT('',#34749);
#6617=VERTEX_POINT('',#34753);
#6618=VERTEX_POINT('',#34755);
#6619=VERTEX_POINT('',#34759);
#6620=VERTEX_POINT('',#34773);
#6621=VERTEX_POINT('',#34775);
#6622=VERTEX_POINT('',#34781);
#6623=VERTEX_POINT('',#34783);
#6624=VERTEX_POINT('',#34787);
#6625=VERTEX_POINT('',#34789);
#6626=VERTEX_POINT('',#34793);
#6627=VERTEX_POINT('',#34795);
#6628=VERTEX_POINT('',#34797);
#6629=VERTEX_POINT('',#34801);
#6630=VERTEX_POINT('',#34803);
#6631=VERTEX_POINT('',#34807);
#6632=VERTEX_POINT('',#34809);
#6633=VERTEX_POINT('',#34816);
#6634=VERTEX_POINT('',#34818);
#6635=VERTEX_POINT('',#34822);
#6636=VERTEX_POINT('',#34824);
#6637=VERTEX_POINT('',#34828);
#6638=VERTEX_POINT('',#34830);
#6639=VERTEX_POINT('',#34837);
#6640=VERTEX_POINT('',#34839);
#6641=VERTEX_POINT('',#34850);
#6642=VERTEX_POINT('',#34851);
#6643=VERTEX_POINT('',#34853);
#6644=VERTEX_POINT('',#34855);
#6645=VERTEX_POINT('',#34857);
#6646=VERTEX_POINT('',#34863);
#6647=VERTEX_POINT('',#34864);
#6648=VERTEX_POINT('',#34866);
#6649=VERTEX_POINT('',#34868);
#6650=VERTEX_POINT('',#34871);
#6651=VERTEX_POINT('',#34876);
#6652=VERTEX_POINT('',#34877);
#6653=VERTEX_POINT('',#34879);
#6654=VERTEX_POINT('',#34881);
#6655=VERTEX_POINT('',#34886);
#6656=VERTEX_POINT('',#34887);
#6657=VERTEX_POINT('',#34891);
#6658=VERTEX_POINT('',#34895);
#6659=VERTEX_POINT('',#34897);
#6660=VERTEX_POINT('',#34899);
#6661=VERTEX_POINT('',#34901);
#6662=VERTEX_POINT('',#34903);
#6663=VERTEX_POINT('',#34906);
#6664=VERTEX_POINT('',#34910);
#6665=VERTEX_POINT('',#34912);
#6666=VERTEX_POINT('',#34916);
#6667=VERTEX_POINT('',#34918);
#6668=VERTEX_POINT('',#34928);
#6669=VERTEX_POINT('',#34930);
#6670=VERTEX_POINT('',#34938);
#6671=VERTEX_POINT('',#34942);
#6672=VERTEX_POINT('',#34944);
#6673=VERTEX_POINT('',#34946);
#6674=VERTEX_POINT('',#34950);
#6675=VERTEX_POINT('',#34952);
#6676=VERTEX_POINT('',#34957);
#6677=VERTEX_POINT('',#34959);
#6678=VERTEX_POINT('',#34963);
#6679=VERTEX_POINT('',#34965);
#6680=VERTEX_POINT('',#34972);
#6681=VERTEX_POINT('',#34976);
#6682=VERTEX_POINT('',#34980);
#6683=VERTEX_POINT('',#34982);
#6684=VERTEX_POINT('',#34986);
#6685=VERTEX_POINT('',#34988);
#6686=VERTEX_POINT('',#34993);
#6687=VERTEX_POINT('',#34997);
#6688=VERTEX_POINT('',#35002);
#6689=VERTEX_POINT('',#35004);
#6690=VERTEX_POINT('',#35006);
#6691=VERTEX_POINT('',#35009);
#6692=VERTEX_POINT('',#35013);
#6693=VERTEX_POINT('',#35017);
#6694=VERTEX_POINT('',#35024);
#6695=VERTEX_POINT('',#35026);
#6696=VERTEX_POINT('',#35030);
#6697=VERTEX_POINT('',#35034);
#6698=VERTEX_POINT('',#35036);
#6699=VERTEX_POINT('',#35038);
#6700=VERTEX_POINT('',#35046);
#6701=VERTEX_POINT('',#35053);
#6702=VERTEX_POINT('',#35059);
#6703=VERTEX_POINT('',#35066);
#6704=VERTEX_POINT('',#35068);
#6705=VERTEX_POINT('',#35072);
#6706=VERTEX_POINT('',#35076);
#6707=VERTEX_POINT('',#35080);
#6708=VERTEX_POINT('',#35084);
#6709=VERTEX_POINT('',#35088);
#6710=VERTEX_POINT('',#35092);
#6711=VERTEX_POINT('',#35106);
#6712=VERTEX_POINT('',#35107);
#6713=VERTEX_POINT('',#35109);
#6714=VERTEX_POINT('',#35111);
#6715=VERTEX_POINT('',#35115);
#6716=VERTEX_POINT('',#35116);
#6717=VERTEX_POINT('',#35118);
#6718=VERTEX_POINT('',#35120);
#6719=VERTEX_POINT('',#35124);
#6720=VERTEX_POINT('',#35125);
#6721=VERTEX_POINT('',#35131);
#6722=VERTEX_POINT('',#35135);
#6723=VERTEX_POINT('',#35142);
#8078=EDGE_CURVE('',#6510,#6511,#5647,.T.);
#8079=EDGE_CURVE('',#6512,#6510,#5648,.T.);
#8080=EDGE_CURVE('',#6513,#6512,#5649,.T.);
#8081=EDGE_CURVE('',#6514,#6513,#1355,.T.);
#8082=EDGE_CURVE('',#6514,#6515,#5650,.T.);
#8083=EDGE_CURVE('',#6515,#6511,#1356,.T.);
#8084=EDGE_CURVE('',#6516,#6516,#5651,.T.);
#8085=EDGE_CURVE('',#6516,#6517,#1357,.T.);
#8086=EDGE_CURVE('',#6517,#6517,#5652,.T.);
#8087=EDGE_CURVE('',#6518,#6519,#5653,.T.);
#8088=EDGE_CURVE('',#6520,#6518,#1358,.T.);
#8089=EDGE_CURVE('',#6520,#6521,#5654,.T.);
#8090=EDGE_CURVE('',#6521,#6519,#1359,.T.);
#8091=EDGE_CURVE('',#6522,#6523,#5655,.T.);
#8092=EDGE_CURVE('',#6524,#6522,#1360,.T.);
#8093=EDGE_CURVE('',#6524,#6525,#5656,.T.);
#8094=EDGE_CURVE('',#6525,#6523,#1361,.T.);
#8095=EDGE_CURVE('',#6526,#6527,#5657,.T.);
#8096=EDGE_CURVE('',#6528,#6526,#1362,.T.);
#8097=EDGE_CURVE('',#6528,#6529,#5658,.T.);
#8098=EDGE_CURVE('',#6529,#6530,#5659,.T.);
#8099=EDGE_CURVE('',#6530,#6527,#1363,.T.);
#8100=EDGE_CURVE('',#6531,#6532,#1364,.T.);
#8101=EDGE_CURVE('',#6533,#6532,#1365,.T.);
#8102=EDGE_CURVE('',#6534,#6533,#1366,.T.);
#8103=EDGE_CURVE('',#6534,#6531,#1367,.T.);
#8104=EDGE_CURVE('',#6535,#6531,#1368,.T.);
#8105=EDGE_CURVE('',#6536,#6534,#1369,.T.);
#8106=EDGE_CURVE('',#6536,#6535,#1370,.T.);
#8107=EDGE_CURVE('',#6537,#6535,#1371,.T.);
#8108=EDGE_CURVE('',#6538,#6536,#1372,.T.);
#8109=EDGE_CURVE('',#6538,#6537,#1373,.T.);
#8110=EDGE_CURVE('',#6539,#6540,#1374,.T.);
#8111=EDGE_CURVE('',#6541,#6539,#1375,.T.);
#8112=EDGE_CURVE('',#6542,#6541,#1376,.T.);
#8113=EDGE_CURVE('',#6540,#6542,#1377,.T.);
#8114=EDGE_CURVE('',#6543,#6544,#1378,.T.);
#8115=EDGE_CURVE('',#6541,#6543,#1379,.T.);
#8116=EDGE_CURVE('',#6539,#6544,#1380,.T.);
#8117=EDGE_CURVE('',#6545,#6546,#1381,.T.);
#8118=EDGE_CURVE('',#6540,#6545,#1382,.T.);
#8119=EDGE_CURVE('',#6542,#6546,#1383,.T.);
#8120=EDGE_CURVE('',#6547,#6548,#1384,.T.);
#8121=EDGE_CURVE('',#6548,#6549,#1385,.T.);
#8122=EDGE_CURVE('',#6549,#6550,#1386,.T.);
#8123=EDGE_CURVE('',#6550,#6547,#1387,.T.);
#8124=EDGE_CURVE('',#6551,#6552,#1388,.T.);
#8125=EDGE_CURVE('',#6551,#6553,#1389,.T.);
#8126=EDGE_CURVE('',#6553,#6554,#1390,.T.);
#8127=EDGE_CURVE('',#6554,#6552,#1391,.T.);
#8128=EDGE_CURVE('',#6549,#6551,#1392,.T.);
#8129=EDGE_CURVE('',#6552,#6555,#1393,.T.);
#8130=EDGE_CURVE('',#6555,#6556,#1394,.T.);
#8131=EDGE_CURVE('',#6550,#6556,#1395,.T.);
#8132=EDGE_CURVE('',#6553,#6548,#1396,.T.);
#8133=EDGE_CURVE('',#6557,#6547,#1397,.T.);
#8134=EDGE_CURVE('',#6558,#6557,#1398,.T.);
#8135=EDGE_CURVE('',#6559,#6558,#1399,.T.);
#8136=EDGE_CURVE('',#6559,#6560,#1400,.T.);
#8137=EDGE_CURVE('',#6560,#6554,#1401,.T.);
#8138=EDGE_CURVE('',#6561,#6562,#1402,.T.);
#8139=EDGE_CURVE('',#6559,#6561,#1403,.T.);
#8140=EDGE_CURVE('',#6558,#6562,#1404,.T.);
#8141=EDGE_CURVE('',#6563,#6564,#1405,.T.);
#8142=EDGE_CURVE('',#6557,#6563,#1406,.T.);
#8143=EDGE_CURVE('',#6547,#6564,#1407,.T.);
#8144=EDGE_CURVE('',#6565,#6566,#5660,.T.);
#8145=EDGE_CURVE('',#6567,#6566,#1408,.T.);
#8146=EDGE_CURVE('',#6550,#6567,#1409,.T.);
#8147=EDGE_CURVE('',#6568,#6556,#1410,.T.);
#8148=EDGE_CURVE('',#6569,#6568,#1411,.T.);
#8149=EDGE_CURVE('',#6569,#6570,#5661,.T.);
#8150=EDGE_CURVE('',#6570,#6565,#1412,.T.);
#8151=EDGE_CURVE('',#6571,#6572,#1413,.T.);
#8152=EDGE_CURVE('',#6573,#6572,#1414,.T.);
#8153=EDGE_CURVE('',#6574,#6573,#1415,.T.);
#8154=EDGE_CURVE('',#6567,#6574,#751,.T.);
#8155=EDGE_CURVE('',#6566,#6571,#752,.T.);
#8156=EDGE_CURVE('',#6575,#6576,#1416,.T.);
#8157=EDGE_CURVE('',#6576,#6577,#1417,.T.);
#8158=EDGE_CURVE('',#6577,#6578,#1418,.T.);
#8159=EDGE_CURVE('',#6578,#6579,#1419,.T.);
#8160=EDGE_CURVE('',#6579,#6580,#1420,.T.);
#8161=EDGE_CURVE('',#6575,#6580,#1421,.T.);
#8162=EDGE_CURVE('',#6581,#6582,#1422,.T.);
#8163=EDGE_CURVE('',#6581,#6583,#1423,.T.);
#8164=EDGE_CURVE('',#6584,#6583,#1424,.T.);
#8165=EDGE_CURVE('',#6584,#6585,#1425,.T.);
#8166=EDGE_CURVE('',#6585,#6586,#1426,.T.);
#8167=EDGE_CURVE('',#6586,#6582,#1427,.T.);
#8168=EDGE_CURVE('',#6585,#6587,#1428,.T.);
#8169=EDGE_CURVE('',#6587,#6588,#1429,.T.);
#8170=EDGE_CURVE('',#6588,#6586,#1430,.T.);
#8171=EDGE_CURVE('',#6589,#6590,#1431,.T.);
#8172=EDGE_CURVE('',#6589,#6591,#1432,.T.);
#8173=EDGE_CURVE('',#6591,#6592,#1433,.T.);
#8174=EDGE_CURVE('',#6592,#6590,#1434,.T.);
#8175=EDGE_CURVE('',#6593,#6594,#1435,.T.);
#8176=EDGE_CURVE('',#6593,#6595,#1436,.T.);
#8177=EDGE_CURVE('',#6595,#6596,#1437,.T.);
#8178=EDGE_CURVE('',#6596,#6592,#1438,.T.);
#8179=EDGE_CURVE('',#6591,#6594,#1439,.T.);
#8180=EDGE_CURVE('',#6587,#6597,#1440,.T.);
#8181=EDGE_CURVE('',#6597,#6584,#1441,.T.);
#8182=EDGE_CURVE('',#6598,#6581,#1442,.T.);
#8183=EDGE_CURVE('',#6599,#6598,#1443,.T.);
#8184=EDGE_CURVE('',#6583,#6599,#1444,.T.);
#8185=EDGE_CURVE('',#6599,#6597,#1445,.T.);
#8186=EDGE_CURVE('',#6600,#6589,#1446,.T.);
#8187=EDGE_CURVE('',#6594,#6600,#1447,.T.);
#8188=EDGE_CURVE('',#6601,#6602,#1448,.T.);
#8189=EDGE_CURVE('',#6595,#6601,#1449,.T.);
#8190=EDGE_CURVE('',#6602,#6593,#1450,.T.);
#8191=EDGE_CURVE('',#6533,#6538,#1451,.T.);
#8192=EDGE_CURVE('',#6603,#6604,#1452,.T.);
#8193=EDGE_CURVE('',#6605,#6603,#5662,.T.);
#8194=EDGE_CURVE('',#6606,#6605,#1453,.T.);
#8195=EDGE_CURVE('',#6604,#6606,#5663,.T.);
#8196=EDGE_CURVE('',#6607,#6605,#1454,.T.);
#8197=EDGE_CURVE('',#6608,#6607,#1455,.T.);
#8198=EDGE_CURVE('',#6606,#6608,#1456,.T.);
#8199=EDGE_CURVE('',#6609,#6604,#1457,.T.);
#8200=EDGE_CURVE('',#6610,#6609,#1458,.T.);
#8201=EDGE_CURVE('',#6603,#6610,#1459,.T.);
#8202=EDGE_CURVE('',#6611,#6607,#5664,.T.);
#8203=EDGE_CURVE('',#6612,#6611,#1460,.T.);
#8204=EDGE_CURVE('',#6608,#6612,#5665,.T.);
#8205=EDGE_CURVE('',#6613,#6609,#5666,.T.);
#8206=EDGE_CURVE('',#6614,#6613,#1461,.T.);
#8207=EDGE_CURVE('',#6610,#6614,#5667,.T.);
#8208=EDGE_CURVE('',#6615,#6611,#1462,.T.);
#8209=EDGE_CURVE('',#6616,#6615,#1463,.T.);
#8210=EDGE_CURVE('',#6612,#6616,#1464,.T.);
#8211=EDGE_CURVE('',#6617,#6613,#1465,.T.);
#8212=EDGE_CURVE('',#6618,#6617,#1466,.T.);
#8213=EDGE_CURVE('',#6614,#6618,#1467,.T.);
#8214=EDGE_CURVE('',#6601,#6619,#1468,.T.);
#8215=EDGE_CURVE('',#6619,#6596,#1469,.T.);
#8216=EDGE_CURVE('',#6618,#6615,#5668,.T.);
#8217=EDGE_CURVE('',#6616,#6617,#5669,.T.);
#8218=EDGE_CURVE('',#6544,#6545,#1470,.T.);
#8219=EDGE_CURVE('',#6555,#6560,#1471,.T.);
#8220=EDGE_CURVE('',#6556,#6559,#1472,.T.);
#8221=EDGE_CURVE('',#6620,#6526,#1473,.T.);
#8222=EDGE_CURVE('',#6621,#6620,#1474,.T.);
#8223=EDGE_CURVE('',#6621,#6512,#1475,.T.);
#8224=EDGE_CURVE('',#6512,#6510,#1476,.T.);
#8225=EDGE_CURVE('',#6510,#6528,#1477,.T.);
#8226=EDGE_CURVE('',#6527,#6622,#1478,.T.);
#8227=EDGE_CURVE('',#6530,#6623,#1479,.T.);
#8228=EDGE_CURVE('',#6623,#6622,#1480,.T.);
#8229=EDGE_CURVE('',#6622,#6624,#5670,.T.);
#8230=EDGE_CURVE('',#6623,#6625,#5671,.T.);
#8231=EDGE_CURVE('',#6625,#6624,#1481,.T.);
#8232=EDGE_CURVE('',#6624,#6626,#1482,.T.);
#8233=EDGE_CURVE('',#6625,#6627,#1483,.T.);
#8234=EDGE_CURVE('',#6627,#6628,#1484,.T.);
#8235=EDGE_CURVE('',#6628,#6626,#1485,.T.);
#8236=EDGE_CURVE('',#6626,#6629,#5672,.T.);
#8237=EDGE_CURVE('',#6628,#6630,#5673,.T.);
#8238=EDGE_CURVE('',#6630,#6629,#1486,.T.);
#8239=EDGE_CURVE('',#6631,#6620,#5674,.T.);
#8240=EDGE_CURVE('',#6632,#6631,#1487,.T.);
#8241=EDGE_CURVE('',#6632,#6621,#5675,.T.);
#8242=EDGE_CURVE('',#6629,#6631,#1488,.T.);
#8243=EDGE_CURVE('',#6630,#6632,#1489,.T.);
#8244=EDGE_CURVE('',#6633,#6522,#5676,.T.);
#8245=EDGE_CURVE('',#6634,#6633,#1490,.T.);
#8246=EDGE_CURVE('',#6634,#6524,#5677,.T.);
#8247=EDGE_CURVE('',#6523,#6635,#5678,.T.);
#8248=EDGE_CURVE('',#6525,#6636,#5679,.T.);
#8249=EDGE_CURVE('',#6636,#6635,#1491,.T.);
#8250=EDGE_CURVE('',#6635,#6637,#1492,.T.);
#8251=EDGE_CURVE('',#6636,#6638,#1493,.T.);
#8252=EDGE_CURVE('',#6638,#6637,#1494,.T.);
#8253=EDGE_CURVE('',#6637,#6518,#5680,.T.);
#8254=EDGE_CURVE('',#6638,#6520,#5681,.T.);
#8255=EDGE_CURVE('',#6519,#6639,#5682,.T.);
#8256=EDGE_CURVE('',#6521,#6640,#5683,.T.);
#8257=EDGE_CURVE('',#6640,#6639,#1495,.T.);
#8258=EDGE_CURVE('',#6511,#6529,#1496,.T.);
#8259=EDGE_CURVE('',#6639,#6633,#1497,.T.);
#8260=EDGE_CURVE('',#6640,#6634,#1498,.T.);
#8261=EDGE_CURVE('',#6641,#6642,#1499,.T.);
#8262=EDGE_CURVE('',#6641,#6643,#5684,.T.);
#8263=EDGE_CURVE('',#6643,#6644,#1500,.T.);
#8264=EDGE_CURVE('',#6644,#6645,#1501,.T.);
#8265=EDGE_CURVE('',#6645,#6642,#1502,.T.);
#8266=EDGE_CURVE('',#6627,#6513,#1503,.T.);
#8267=EDGE_CURVE('',#6646,#6647,#1504,.T.);
#8268=EDGE_CURVE('',#6648,#6646,#1505,.T.);
#8269=EDGE_CURVE('',#6649,#6648,#1506,.T.);
#8270=EDGE_CURVE('',#6529,#6649,#1507,.T.);
#8271=EDGE_CURVE('',#6515,#6650,#1508,.T.);
#8272=EDGE_CURVE('',#6650,#6647,#1509,.T.);
#8273=EDGE_CURVE('',#6651,#6652,#1510,.T.);
#8274=EDGE_CURVE('',#6652,#6653,#1511,.T.);
#8275=EDGE_CURVE('',#6654,#6653,#1512,.T.);
#8276=EDGE_CURVE('',#6654,#6647,#1513,.T.);
#8277=EDGE_CURVE('',#6650,#6651,#1514,.T.);
#8278=EDGE_CURVE('',#6655,#6656,#1515,.T.);
#8279=EDGE_CURVE('',#6656,#6580,#1516,.T.);
#8280=EDGE_CURVE('',#6579,#6514,#1517,.T.);
#8281=EDGE_CURVE('',#6657,#6627,#1518,.T.);
#8282=EDGE_CURVE('',#6657,#6655,#1519,.T.);
#8283=EDGE_CURVE('',#6658,#6649,#1520,.T.);
#8284=EDGE_CURVE('',#6659,#6658,#1521,.T.);
#8285=EDGE_CURVE('',#6659,#6660,#1522,.T.);
#8286=EDGE_CURVE('',#6661,#6660,#1523,.T.);
#8287=EDGE_CURVE('',#6661,#6662,#1524,.T.);
#8288=EDGE_CURVE('',#6662,#6641,#1525,.T.);
#8289=EDGE_CURVE('',#6642,#6663,#1526,.T.);
#8290=EDGE_CURVE('',#6663,#6657,#1527,.T.);
#8291=EDGE_CURVE('',#6664,#6578,#1528,.T.);
#8292=EDGE_CURVE('',#6665,#6664,#1529,.T.);
#8293=EDGE_CURVE('',#6651,#6665,#1530,.T.);
#8294=EDGE_CURVE('',#6666,#6655,#1531,.T.);
#8295=EDGE_CURVE('',#6666,#6667,#1532,.T.);
#8296=EDGE_CURVE('',#6667,#6656,#1533,.T.);
#8297=EDGE_CURVE('',#6667,#6575,#1534,.T.);
#8298=EDGE_CURVE('',#6663,#6666,#1535,.T.);
#8299=EDGE_CURVE('',#6576,#6645,#1536,.T.);
#8300=EDGE_CURVE('',#6668,#6646,#1537,.T.);
#8301=EDGE_CURVE('',#6669,#6668,#1538,.T.);
#8302=EDGE_CURVE('',#6669,#6648,#1539,.T.);
#8303=EDGE_CURVE('',#6668,#6654,#1540,.T.);
#8304=EDGE_CURVE('',#6658,#6669,#1541,.T.);
#8305=EDGE_CURVE('',#6653,#6670,#1542,.T.);
#8306=EDGE_CURVE('',#6670,#6659,#1543,.T.);
#8307=EDGE_CURVE('',#6671,#6652,#1544,.T.);
#8308=EDGE_CURVE('',#6671,#6672,#1545,.T.);
#8309=EDGE_CURVE('',#6672,#6673,#1546,.T.);
#8310=EDGE_CURVE('',#6653,#6673,#1547,.T.);
#8311=EDGE_CURVE('',#6673,#6674,#1548,.T.);
#8312=EDGE_CURVE('',#6672,#6675,#1549,.T.);
#8313=EDGE_CURVE('',#6675,#6674,#1550,.T.);
#8314=EDGE_CURVE('',#6674,#6670,#1551,.T.);
#8315=EDGE_CURVE('',#6675,#6676,#1552,.T.);
#8316=EDGE_CURVE('',#6676,#6677,#1553,.T.);
#8317=EDGE_CURVE('',#6670,#6677,#1554,.T.);
#8318=EDGE_CURVE('',#6677,#6678,#1555,.T.);
#8319=EDGE_CURVE('',#6676,#6679,#1556,.T.);
#8320=EDGE_CURVE('',#6679,#6678,#1557,.T.);
#8321=EDGE_CURVE('',#6678,#6660,#5685,.T.);
#8322=EDGE_CURVE('',#6679,#6661,#5686,.T.);
#8323=EDGE_CURVE('',#6662,#6680,#5687,.T.);
#8324=EDGE_CURVE('',#6680,#6643,#1558,.T.);
#8325=EDGE_CURVE('',#6680,#6681,#1559,.T.);
#8326=EDGE_CURVE('',#6681,#6644,#1560,.T.);
#8327=EDGE_CURVE('',#6681,#6682,#1561,.T.);
#8328=EDGE_CURVE('',#6682,#6683,#1562,.T.);
#8329=EDGE_CURVE('',#6645,#6683,#1563,.T.);
#8330=EDGE_CURVE('',#6683,#6684,#1564,.T.);
#8331=EDGE_CURVE('',#6682,#6685,#1565,.T.);
#8332=EDGE_CURVE('',#6685,#6684,#1566,.T.);
#8333=EDGE_CURVE('',#6684,#6576,#1567,.T.);
#8334=EDGE_CURVE('',#6685,#6686,#1568,.T.);
#8335=EDGE_CURVE('',#6686,#6577,#1569,.T.);
#8336=EDGE_CURVE('',#6571,#6687,#1570,.T.);
#8337=EDGE_CURVE('',#6578,#6687,#1571,.T.);
#8338=EDGE_CURVE('',#6686,#6572,#1572,.T.);
#8339=EDGE_CURVE('',#6688,#6561,#1573,.T.);
#8340=EDGE_CURVE('',#6562,#6689,#1574,.T.);
#8341=EDGE_CURVE('',#6689,#6690,#5688,.T.);
#8342=EDGE_CURVE('',#6690,#6651,#1575,.T.);
#8343=EDGE_CURVE('',#6665,#6691,#1576,.T.);
#8344=EDGE_CURVE('',#6691,#6688,#5689,.T.);
#8345=EDGE_CURVE('',#6565,#6692,#1577,.T.);
#8346=EDGE_CURVE('',#6687,#6692,#5690,.T.);
#8347=EDGE_CURVE('',#6693,#6569,#753,.T.);
#8348=EDGE_CURVE('',#6693,#6690,#1578,.T.);
#8349=EDGE_CURVE('',#6570,#6689,#1579,.T.);
#8350=EDGE_CURVE('',#6692,#6563,#1580,.T.);
#8351=EDGE_CURVE('',#6564,#6694,#1581,.T.);
#8352=EDGE_CURVE('',#6694,#6695,#5691,.T.);
#8353=EDGE_CURVE('',#6695,#6664,#1582,.T.);
#8354=EDGE_CURVE('',#6696,#6693,#1583,.T.);
#8355=EDGE_CURVE('',#6696,#6671,#1584,.T.);
#8356=EDGE_CURVE('',#6696,#6697,#1585,.T.);
#8357=EDGE_CURVE('',#6698,#6697,#1586,.T.);
#8358=EDGE_CURVE('',#6699,#6698,#1587,.T.);
#8359=EDGE_CURVE('',#6573,#6699,#1588,.T.);
#8360=EDGE_CURVE('',#6688,#6568,#1589,.T.);
#8361=EDGE_CURVE('',#6691,#6700,#1590,.T.);
#8362=EDGE_CURVE('',#6700,#6568,#754,.T.);
#8363=EDGE_CURVE('',#6694,#6567,#1591,.T.);
#8364=EDGE_CURVE('',#6695,#6574,#1592,.T.);
#8365=EDGE_CURVE('',#6701,#6699,#1593,.T.);
#8366=EDGE_CURVE('',#6664,#6701,#1594,.T.);
#8367=EDGE_CURVE('',#6697,#6700,#1595,.T.);
#8368=EDGE_CURVE('',#6702,#6665,#1596,.T.);
#8369=EDGE_CURVE('',#6702,#6698,#1597,.T.);
#8370=EDGE_CURVE('',#6701,#6702,#1598,.T.);
#8371=EDGE_CURVE('',#6703,#6606,#1599,.T.);
#8372=EDGE_CURVE('',#6704,#6608,#1600,.T.);
#8373=EDGE_CURVE('',#6703,#6704,#1601,.T.);
#8374=EDGE_CURVE('',#6705,#6612,#1602,.T.);
#8375=EDGE_CURVE('',#6704,#6705,#5692,.T.);
#8376=EDGE_CURVE('',#6706,#6616,#1603,.T.);
#8377=EDGE_CURVE('',#6705,#6706,#1604,.T.);
#8378=EDGE_CURVE('',#6707,#6617,#1605,.T.);
#8379=EDGE_CURVE('',#6706,#6707,#5693,.T.);
#8380=EDGE_CURVE('',#6708,#6613,#1606,.T.);
#8381=EDGE_CURVE('',#6707,#6708,#1607,.T.);
#8382=EDGE_CURVE('',#6709,#6609,#1608,.T.);
#8383=EDGE_CURVE('',#6708,#6709,#5694,.T.);
#8384=EDGE_CURVE('',#6710,#6604,#1609,.T.);
#8385=EDGE_CURVE('',#6710,#6703,#5695,.T.);
#8386=EDGE_CURVE('',#6546,#6710,#1610,.T.);
#8387=EDGE_CURVE('',#6537,#6543,#1611,.T.);
#8388=EDGE_CURVE('',#6709,#6532,#1612,.T.);
#8389=EDGE_CURVE('',#6600,#6602,#1613,.T.);
#8390=EDGE_CURVE('',#6590,#6619,#1614,.T.);
#8391=EDGE_CURVE('',#6711,#6712,#1615,.T.);
#8392=EDGE_CURVE('',#6711,#6713,#1616,.T.);
#8393=EDGE_CURVE('',#6713,#6714,#1617,.T.);
#8394=EDGE_CURVE('',#6714,#6712,#1618,.T.);
#8395=EDGE_CURVE('',#6715,#6716,#1619,.T.);
#8396=EDGE_CURVE('',#6715,#6717,#1620,.T.);
#8397=EDGE_CURVE('',#6717,#6718,#1621,.T.);
#8398=EDGE_CURVE('',#6718,#6716,#1622,.T.);
#8399=EDGE_CURVE('',#6719,#6720,#1623,.T.);
#8400=EDGE_CURVE('',#6719,#6715,#1624,.T.);
#8401=EDGE_CURVE('',#6716,#6714,#1625,.T.);
#8402=EDGE_CURVE('',#6713,#6720,#1626,.T.);
#8403=EDGE_CURVE('',#6717,#6721,#1627,.T.);
#8404=EDGE_CURVE('',#6721,#6719,#1628,.T.);
#8405=EDGE_CURVE('',#6722,#6721,#1629,.T.);
#8406=EDGE_CURVE('',#6720,#6722,#1630,.T.);
#8407=EDGE_CURVE('',#6722,#6711,#1631,.T.);
#8408=EDGE_CURVE('',#6712,#6718,#1632,.T.);
#8409=EDGE_CURVE('',#6598,#6723,#1633,.T.);
#8410=EDGE_CURVE('',#6582,#6723,#1634,.T.);
#8411=EDGE_CURVE('',#6723,#6588,#1635,.T.);
#10743=ORIENTED_EDGE('',*,*,#8078,.F.);
#10744=ORIENTED_EDGE('',*,*,#8079,.F.);
#10745=ORIENTED_EDGE('',*,*,#8080,.F.);
#10746=ORIENTED_EDGE('',*,*,#8081,.F.);
#10747=ORIENTED_EDGE('',*,*,#8082,.T.);
#10748=ORIENTED_EDGE('',*,*,#8083,.T.);
#10749=ORIENTED_EDGE('',*,*,#8084,.F.);
#10750=ORIENTED_EDGE('',*,*,#8085,.T.);
#10751=ORIENTED_EDGE('',*,*,#8086,.T.);
#10752=ORIENTED_EDGE('',*,*,#8085,.F.);
#10753=ORIENTED_EDGE('',*,*,#8087,.F.);
#10754=ORIENTED_EDGE('',*,*,#8088,.F.);
#10755=ORIENTED_EDGE('',*,*,#8089,.T.);
#10756=ORIENTED_EDGE('',*,*,#8090,.T.);
#10757=ORIENTED_EDGE('',*,*,#8091,.F.);
#10758=ORIENTED_EDGE('',*,*,#8092,.F.);
#10759=ORIENTED_EDGE('',*,*,#8093,.T.);
#10760=ORIENTED_EDGE('',*,*,#8094,.T.);
#10761=ORIENTED_EDGE('',*,*,#8095,.F.);
#10762=ORIENTED_EDGE('',*,*,#8096,.F.);
#10763=ORIENTED_EDGE('',*,*,#8097,.T.);
#10764=ORIENTED_EDGE('',*,*,#8098,.T.);
#10765=ORIENTED_EDGE('',*,*,#8099,.T.);
#10766=ORIENTED_EDGE('',*,*,#8100,.T.);
#10767=ORIENTED_EDGE('',*,*,#8101,.F.);
#10768=ORIENTED_EDGE('',*,*,#8102,.F.);
#10769=ORIENTED_EDGE('',*,*,#8103,.T.);
#10770=ORIENTED_EDGE('',*,*,#8104,.T.);
#10771=ORIENTED_EDGE('',*,*,#8103,.F.);
#10772=ORIENTED_EDGE('',*,*,#8105,.F.);
#10773=ORIENTED_EDGE('',*,*,#8106,.T.);
#10774=ORIENTED_EDGE('',*,*,#8107,.T.);
#10775=ORIENTED_EDGE('',*,*,#8106,.F.);
#10776=ORIENTED_EDGE('',*,*,#8108,.F.);
#10777=ORIENTED_EDGE('',*,*,#8109,.T.);
#10778=ORIENTED_EDGE('',*,*,#8110,.F.);
#10779=ORIENTED_EDGE('',*,*,#8111,.F.);
#10780=ORIENTED_EDGE('',*,*,#8112,.F.);
#10781=ORIENTED_EDGE('',*,*,#8113,.F.);
#10782=ORIENTED_EDGE('',*,*,#8114,.F.);
#10783=ORIENTED_EDGE('',*,*,#8115,.F.);
#10784=ORIENTED_EDGE('',*,*,#8111,.T.);
#10785=ORIENTED_EDGE('',*,*,#8116,.T.);
#10786=ORIENTED_EDGE('',*,*,#8117,.F.);
#10787=ORIENTED_EDGE('',*,*,#8118,.F.);
#10788=ORIENTED_EDGE('',*,*,#8113,.T.);
#10789=ORIENTED_EDGE('',*,*,#8119,.T.);
#10790=ORIENTED_EDGE('',*,*,#8120,.T.);
#10791=ORIENTED_EDGE('',*,*,#8121,.T.);
#10792=ORIENTED_EDGE('',*,*,#8122,.T.);
#10793=ORIENTED_EDGE('',*,*,#8123,.T.);
#10794=ORIENTED_EDGE('',*,*,#8124,.F.);
#10795=ORIENTED_EDGE('',*,*,#8125,.T.);
#10796=ORIENTED_EDGE('',*,*,#8126,.T.);
#10797=ORIENTED_EDGE('',*,*,#8127,.T.);
#10798=ORIENTED_EDGE('',*,*,#8122,.F.);
#10799=ORIENTED_EDGE('',*,*,#8128,.T.);
#10800=ORIENTED_EDGE('',*,*,#8124,.T.);
#10801=ORIENTED_EDGE('',*,*,#8129,.T.);
#10802=ORIENTED_EDGE('',*,*,#8130,.T.);
#10803=ORIENTED_EDGE('',*,*,#8131,.F.);
#10804=ORIENTED_EDGE('',*,*,#8126,.F.);
#10805=ORIENTED_EDGE('',*,*,#8132,.T.);
#10806=ORIENTED_EDGE('',*,*,#8120,.F.);
#10807=ORIENTED_EDGE('',*,*,#8133,.F.);
#10808=ORIENTED_EDGE('',*,*,#8134,.F.);
#10809=ORIENTED_EDGE('',*,*,#8135,.F.);
#10810=ORIENTED_EDGE('',*,*,#8136,.T.);
#10811=ORIENTED_EDGE('',*,*,#8137,.T.);
#10812=ORIENTED_EDGE('',*,*,#8138,.F.);
#10813=ORIENTED_EDGE('',*,*,#8139,.F.);
#10814=ORIENTED_EDGE('',*,*,#8135,.T.);
#10815=ORIENTED_EDGE('',*,*,#8140,.T.);
#10816=ORIENTED_EDGE('',*,*,#8141,.F.);
#10817=ORIENTED_EDGE('',*,*,#8142,.F.);
#10818=ORIENTED_EDGE('',*,*,#8133,.T.);
#10819=ORIENTED_EDGE('',*,*,#8143,.T.);
#10820=ORIENTED_EDGE('',*,*,#8144,.T.);
#10821=ORIENTED_EDGE('',*,*,#8145,.F.);
#10822=ORIENTED_EDGE('',*,*,#8146,.F.);
#10823=ORIENTED_EDGE('',*,*,#8131,.T.);
#10824=ORIENTED_EDGE('',*,*,#8147,.F.);
#10825=ORIENTED_EDGE('',*,*,#8148,.F.);
#10826=ORIENTED_EDGE('',*,*,#8149,.T.);
#10827=ORIENTED_EDGE('',*,*,#8150,.T.);
#10828=ORIENTED_EDGE('',*,*,#8151,.T.);
#10829=ORIENTED_EDGE('',*,*,#8152,.F.);
#10830=ORIENTED_EDGE('',*,*,#8153,.F.);
#10831=ORIENTED_EDGE('',*,*,#8154,.F.);
#10832=ORIENTED_EDGE('',*,*,#8145,.T.);
#10833=ORIENTED_EDGE('',*,*,#8155,.T.);
#10834=ORIENTED_EDGE('',*,*,#8156,.T.);
#10835=ORIENTED_EDGE('',*,*,#8157,.T.);
#10836=ORIENTED_EDGE('',*,*,#8158,.T.);
#10837=ORIENTED_EDGE('',*,*,#8159,.T.);
#10838=ORIENTED_EDGE('',*,*,#8160,.T.);
#10839=ORIENTED_EDGE('',*,*,#8161,.F.);
#10840=ORIENTED_EDGE('',*,*,#8162,.F.);
#10841=ORIENTED_EDGE('',*,*,#8163,.T.);
#10842=ORIENTED_EDGE('',*,*,#8164,.F.);
#10843=ORIENTED_EDGE('',*,*,#8165,.T.);
#10844=ORIENTED_EDGE('',*,*,#8166,.T.);
#10845=ORIENTED_EDGE('',*,*,#8167,.T.);
#10846=ORIENTED_EDGE('',*,*,#8166,.F.);
#10847=ORIENTED_EDGE('',*,*,#8168,.T.);
#10848=ORIENTED_EDGE('',*,*,#8169,.T.);
#10849=ORIENTED_EDGE('',*,*,#8170,.T.);
#10850=ORIENTED_EDGE('',*,*,#8171,.F.);
#10851=ORIENTED_EDGE('',*,*,#8172,.T.);
#10852=ORIENTED_EDGE('',*,*,#8173,.T.);
#10853=ORIENTED_EDGE('',*,*,#8174,.T.);
#10854=ORIENTED_EDGE('',*,*,#8175,.F.);
#10855=ORIENTED_EDGE('',*,*,#8176,.T.);
#10856=ORIENTED_EDGE('',*,*,#8177,.T.);
#10857=ORIENTED_EDGE('',*,*,#8178,.T.);
#10858=ORIENTED_EDGE('',*,*,#8173,.F.);
#10859=ORIENTED_EDGE('',*,*,#8179,.T.);
#10860=ORIENTED_EDGE('',*,*,#8180,.F.);
#10861=ORIENTED_EDGE('',*,*,#8168,.F.);
#10862=ORIENTED_EDGE('',*,*,#8165,.F.);
#10863=ORIENTED_EDGE('',*,*,#8181,.F.);
#10864=ORIENTED_EDGE('',*,*,#8163,.F.);
#10865=ORIENTED_EDGE('',*,*,#8182,.F.);
#10866=ORIENTED_EDGE('',*,*,#8183,.F.);
#10867=ORIENTED_EDGE('',*,*,#8184,.F.);
#10868=ORIENTED_EDGE('',*,*,#8164,.T.);
#10869=ORIENTED_EDGE('',*,*,#8184,.T.);
#10870=ORIENTED_EDGE('',*,*,#8185,.T.);
#10871=ORIENTED_EDGE('',*,*,#8181,.T.);
#10872=ORIENTED_EDGE('',*,*,#8179,.F.);
#10873=ORIENTED_EDGE('',*,*,#8172,.F.);
#10874=ORIENTED_EDGE('',*,*,#8186,.F.);
#10875=ORIENTED_EDGE('',*,*,#8187,.F.);
#10876=ORIENTED_EDGE('',*,*,#8188,.F.);
#10877=ORIENTED_EDGE('',*,*,#8189,.F.);
#10878=ORIENTED_EDGE('',*,*,#8176,.F.);
#10879=ORIENTED_EDGE('',*,*,#8190,.F.);
#10880=ORIENTED_EDGE('',*,*,#8108,.T.);
#10881=ORIENTED_EDGE('',*,*,#8105,.T.);
#10882=ORIENTED_EDGE('',*,*,#8102,.T.);
#10883=ORIENTED_EDGE('',*,*,#8191,.T.);
#10884=ORIENTED_EDGE('',*,*,#8192,.F.);
#10885=ORIENTED_EDGE('',*,*,#8193,.F.);
#10886=ORIENTED_EDGE('',*,*,#8194,.F.);
#10887=ORIENTED_EDGE('',*,*,#8195,.F.);
#10888=ORIENTED_EDGE('',*,*,#8194,.T.);
#10889=ORIENTED_EDGE('',*,*,#8196,.F.);
#10890=ORIENTED_EDGE('',*,*,#8197,.F.);
#10891=ORIENTED_EDGE('',*,*,#8198,.F.);
#10892=ORIENTED_EDGE('',*,*,#8192,.T.);
#10893=ORIENTED_EDGE('',*,*,#8199,.F.);
#10894=ORIENTED_EDGE('',*,*,#8200,.F.);
#10895=ORIENTED_EDGE('',*,*,#8201,.F.);
#10896=ORIENTED_EDGE('',*,*,#8197,.T.);
#10897=ORIENTED_EDGE('',*,*,#8202,.F.);
#10898=ORIENTED_EDGE('',*,*,#8203,.F.);
#10899=ORIENTED_EDGE('',*,*,#8204,.F.);
#10900=ORIENTED_EDGE('',*,*,#8200,.T.);
#10901=ORIENTED_EDGE('',*,*,#8205,.F.);
#10902=ORIENTED_EDGE('',*,*,#8206,.F.);
#10903=ORIENTED_EDGE('',*,*,#8207,.F.);
#10904=ORIENTED_EDGE('',*,*,#8203,.T.);
#10905=ORIENTED_EDGE('',*,*,#8208,.F.);
#10906=ORIENTED_EDGE('',*,*,#8209,.F.);
#10907=ORIENTED_EDGE('',*,*,#8210,.F.);
#10908=ORIENTED_EDGE('',*,*,#8206,.T.);
#10909=ORIENTED_EDGE('',*,*,#8211,.F.);
#10910=ORIENTED_EDGE('',*,*,#8212,.F.);
#10911=ORIENTED_EDGE('',*,*,#8213,.F.);
#10912=ORIENTED_EDGE('',*,*,#8177,.F.);
#10913=ORIENTED_EDGE('',*,*,#8189,.T.);
#10914=ORIENTED_EDGE('',*,*,#8214,.T.);
#10915=ORIENTED_EDGE('',*,*,#8215,.T.);
#10916=ORIENTED_EDGE('',*,*,#8209,.T.);
#10917=ORIENTED_EDGE('',*,*,#8216,.F.);
#10918=ORIENTED_EDGE('',*,*,#8212,.T.);
#10919=ORIENTED_EDGE('',*,*,#8217,.F.);
#10920=ORIENTED_EDGE('',*,*,#8218,.F.);
#10921=ORIENTED_EDGE('',*,*,#8116,.F.);
#10922=ORIENTED_EDGE('',*,*,#8110,.T.);
#10923=ORIENTED_EDGE('',*,*,#8118,.T.);
#10924=ORIENTED_EDGE('',*,*,#8130,.F.);
#10925=ORIENTED_EDGE('',*,*,#8219,.T.);
#10926=ORIENTED_EDGE('',*,*,#8136,.F.);
#10927=ORIENTED_EDGE('',*,*,#8220,.F.);
#10928=ORIENTED_EDGE('',*,*,#8137,.F.);
#10929=ORIENTED_EDGE('',*,*,#8219,.F.);
#10930=ORIENTED_EDGE('',*,*,#8129,.F.);
#10931=ORIENTED_EDGE('',*,*,#8127,.F.);
#10932=ORIENTED_EDGE('',*,*,#8132,.F.);
#10933=ORIENTED_EDGE('',*,*,#8125,.F.);
#10934=ORIENTED_EDGE('',*,*,#8128,.F.);
#10935=ORIENTED_EDGE('',*,*,#8121,.F.);
#10936=ORIENTED_EDGE('',*,*,#8221,.F.);
#10937=ORIENTED_EDGE('',*,*,#8222,.F.);
#10938=ORIENTED_EDGE('',*,*,#8223,.T.);
#10939=ORIENTED_EDGE('',*,*,#8224,.T.);
#10940=ORIENTED_EDGE('',*,*,#8225,.T.);
#10941=ORIENTED_EDGE('',*,*,#8096,.T.);
#10942=ORIENTED_EDGE('',*,*,#8226,.F.);
#10943=ORIENTED_EDGE('',*,*,#8099,.F.);
#10944=ORIENTED_EDGE('',*,*,#8227,.T.);
#10945=ORIENTED_EDGE('',*,*,#8228,.T.);
#10946=ORIENTED_EDGE('',*,*,#8229,.F.);
#10947=ORIENTED_EDGE('',*,*,#8228,.F.);
#10948=ORIENTED_EDGE('',*,*,#8230,.T.);
#10949=ORIENTED_EDGE('',*,*,#8231,.T.);
#10950=ORIENTED_EDGE('',*,*,#8232,.F.);
#10951=ORIENTED_EDGE('',*,*,#8231,.F.);
#10952=ORIENTED_EDGE('',*,*,#8233,.T.);
#10953=ORIENTED_EDGE('',*,*,#8234,.T.);
#10954=ORIENTED_EDGE('',*,*,#8235,.T.);
#10955=ORIENTED_EDGE('',*,*,#8236,.F.);
#10956=ORIENTED_EDGE('',*,*,#8235,.F.);
#10957=ORIENTED_EDGE('',*,*,#8237,.T.);
#10958=ORIENTED_EDGE('',*,*,#8238,.T.);
#10959=ORIENTED_EDGE('',*,*,#8239,.F.);
#10960=ORIENTED_EDGE('',*,*,#8240,.F.);
#10961=ORIENTED_EDGE('',*,*,#8241,.T.);
#10962=ORIENTED_EDGE('',*,*,#8222,.T.);
#10963=ORIENTED_EDGE('',*,*,#8242,.F.);
#10964=ORIENTED_EDGE('',*,*,#8238,.F.);
#10965=ORIENTED_EDGE('',*,*,#8243,.T.);
#10966=ORIENTED_EDGE('',*,*,#8240,.T.);
#10967=ORIENTED_EDGE('',*,*,#8244,.F.);
#10968=ORIENTED_EDGE('',*,*,#8245,.F.);
#10969=ORIENTED_EDGE('',*,*,#8246,.T.);
#10970=ORIENTED_EDGE('',*,*,#8092,.T.);
#10971=ORIENTED_EDGE('',*,*,#8247,.F.);
#10972=ORIENTED_EDGE('',*,*,#8094,.F.);
#10973=ORIENTED_EDGE('',*,*,#8248,.T.);
#10974=ORIENTED_EDGE('',*,*,#8249,.T.);
#10975=ORIENTED_EDGE('',*,*,#8250,.F.);
#10976=ORIENTED_EDGE('',*,*,#8249,.F.);
#10977=ORIENTED_EDGE('',*,*,#8251,.T.);
#10978=ORIENTED_EDGE('',*,*,#8252,.T.);
#10979=ORIENTED_EDGE('',*,*,#8253,.F.);
#10980=ORIENTED_EDGE('',*,*,#8252,.F.);
#10981=ORIENTED_EDGE('',*,*,#8254,.T.);
#10982=ORIENTED_EDGE('',*,*,#8088,.T.);
#10983=ORIENTED_EDGE('',*,*,#8255,.F.);
#10984=ORIENTED_EDGE('',*,*,#8090,.F.);
#10985=ORIENTED_EDGE('',*,*,#8256,.T.);
#10986=ORIENTED_EDGE('',*,*,#8257,.T.);
#10987=ORIENTED_EDGE('',*,*,#8078,.T.);
#10988=ORIENTED_EDGE('',*,*,#8258,.T.);
#10989=ORIENTED_EDGE('',*,*,#8097,.F.);
#10990=ORIENTED_EDGE('',*,*,#8225,.F.);
#10991=ORIENTED_EDGE('',*,*,#8239,.T.);
#10992=ORIENTED_EDGE('',*,*,#8221,.T.);
#10993=ORIENTED_EDGE('',*,*,#8095,.T.);
#10994=ORIENTED_EDGE('',*,*,#8226,.T.);
#10995=ORIENTED_EDGE('',*,*,#8229,.T.);
#10996=ORIENTED_EDGE('',*,*,#8232,.T.);
#10997=ORIENTED_EDGE('',*,*,#8236,.T.);
#10998=ORIENTED_EDGE('',*,*,#8242,.T.);
#10999=ORIENTED_EDGE('',*,*,#8259,.T.);
#11000=ORIENTED_EDGE('',*,*,#8244,.T.);
#11001=ORIENTED_EDGE('',*,*,#8091,.T.);
#11002=ORIENTED_EDGE('',*,*,#8247,.T.);
#11003=ORIENTED_EDGE('',*,*,#8250,.T.);
#11004=ORIENTED_EDGE('',*,*,#8253,.T.);
#11005=ORIENTED_EDGE('',*,*,#8087,.T.);
#11006=ORIENTED_EDGE('',*,*,#8255,.T.);
#11007=ORIENTED_EDGE('',*,*,#8246,.F.);
#11008=ORIENTED_EDGE('',*,*,#8260,.F.);
#11009=ORIENTED_EDGE('',*,*,#8256,.F.);
#11010=ORIENTED_EDGE('',*,*,#8089,.F.);
#11011=ORIENTED_EDGE('',*,*,#8254,.F.);
#11012=ORIENTED_EDGE('',*,*,#8251,.F.);
#11013=ORIENTED_EDGE('',*,*,#8248,.F.);
#11014=ORIENTED_EDGE('',*,*,#8093,.F.);
#11015=ORIENTED_EDGE('',*,*,#8084,.T.);
#11016=ORIENTED_EDGE('',*,*,#8259,.F.);
#11017=ORIENTED_EDGE('',*,*,#8257,.F.);
#11018=ORIENTED_EDGE('',*,*,#8260,.T.);
#11019=ORIENTED_EDGE('',*,*,#8245,.T.);
#11020=ORIENTED_EDGE('',*,*,#8261,.F.);
#11021=ORIENTED_EDGE('',*,*,#8262,.T.);
#11022=ORIENTED_EDGE('',*,*,#8263,.T.);
#11023=ORIENTED_EDGE('',*,*,#8264,.T.);
#11024=ORIENTED_EDGE('',*,*,#8265,.T.);
#11025=ORIENTED_EDGE('',*,*,#8234,.F.);
#11026=ORIENTED_EDGE('',*,*,#8266,.T.);
#11027=ORIENTED_EDGE('',*,*,#8080,.T.);
#11028=ORIENTED_EDGE('',*,*,#8223,.F.);
#11029=ORIENTED_EDGE('',*,*,#8241,.F.);
#11030=ORIENTED_EDGE('',*,*,#8243,.F.);
#11031=ORIENTED_EDGE('',*,*,#8237,.F.);
#11032=ORIENTED_EDGE('',*,*,#8086,.F.);
#11033=ORIENTED_EDGE('',*,*,#8267,.F.);
#11034=ORIENTED_EDGE('',*,*,#8268,.F.);
#11035=ORIENTED_EDGE('',*,*,#8269,.F.);
#11036=ORIENTED_EDGE('',*,*,#8270,.F.);
#11037=ORIENTED_EDGE('',*,*,#8258,.F.);
#11038=ORIENTED_EDGE('',*,*,#8083,.F.);
#11039=ORIENTED_EDGE('',*,*,#8271,.T.);
#11040=ORIENTED_EDGE('',*,*,#8272,.T.);
#11041=ORIENTED_EDGE('',*,*,#8224,.F.);
#11042=ORIENTED_EDGE('',*,*,#8079,.T.);
#11043=ORIENTED_EDGE('',*,*,#8273,.T.);
#11044=ORIENTED_EDGE('',*,*,#8274,.T.);
#11045=ORIENTED_EDGE('',*,*,#8275,.F.);
#11046=ORIENTED_EDGE('',*,*,#8276,.T.);
#11047=ORIENTED_EDGE('',*,*,#8272,.F.);
#11048=ORIENTED_EDGE('',*,*,#8277,.T.);
#11049=ORIENTED_EDGE('',*,*,#8278,.T.);
#11050=ORIENTED_EDGE('',*,*,#8279,.T.);
#11051=ORIENTED_EDGE('',*,*,#8160,.F.);
#11052=ORIENTED_EDGE('',*,*,#8280,.T.);
#11053=ORIENTED_EDGE('',*,*,#8081,.T.);
#11054=ORIENTED_EDGE('',*,*,#8266,.F.);
#11055=ORIENTED_EDGE('',*,*,#8281,.F.);
#11056=ORIENTED_EDGE('',*,*,#8282,.T.);
#11057=ORIENTED_EDGE('',*,*,#8283,.F.);
#11058=ORIENTED_EDGE('',*,*,#8284,.F.);
#11059=ORIENTED_EDGE('',*,*,#8285,.T.);
#11060=ORIENTED_EDGE('',*,*,#8286,.F.);
#11061=ORIENTED_EDGE('',*,*,#8287,.T.);
#11062=ORIENTED_EDGE('',*,*,#8288,.T.);
#11063=ORIENTED_EDGE('',*,*,#8261,.T.);
#11064=ORIENTED_EDGE('',*,*,#8289,.T.);
#11065=ORIENTED_EDGE('',*,*,#8290,.T.);
#11066=ORIENTED_EDGE('',*,*,#8281,.T.);
#11067=ORIENTED_EDGE('',*,*,#8233,.F.);
#11068=ORIENTED_EDGE('',*,*,#8230,.F.);
#11069=ORIENTED_EDGE('',*,*,#8227,.F.);
#11070=ORIENTED_EDGE('',*,*,#8098,.F.);
#11071=ORIENTED_EDGE('',*,*,#8270,.T.);
#11072=ORIENTED_EDGE('',*,*,#8271,.F.);
#11073=ORIENTED_EDGE('',*,*,#8082,.F.);
#11074=ORIENTED_EDGE('',*,*,#8280,.F.);
#11075=ORIENTED_EDGE('',*,*,#8159,.F.);
#11076=ORIENTED_EDGE('',*,*,#8291,.F.);
#11077=ORIENTED_EDGE('',*,*,#8292,.F.);
#11078=ORIENTED_EDGE('',*,*,#8293,.F.);
#11079=ORIENTED_EDGE('',*,*,#8277,.F.);
#11080=ORIENTED_EDGE('',*,*,#8278,.F.);
#11081=ORIENTED_EDGE('',*,*,#8294,.F.);
#11082=ORIENTED_EDGE('',*,*,#8295,.T.);
#11083=ORIENTED_EDGE('',*,*,#8296,.T.);
#11084=ORIENTED_EDGE('',*,*,#8279,.F.);
#11085=ORIENTED_EDGE('',*,*,#8296,.F.);
#11086=ORIENTED_EDGE('',*,*,#8297,.T.);
#11087=ORIENTED_EDGE('',*,*,#8161,.T.);
#11088=ORIENTED_EDGE('',*,*,#8282,.F.);
#11089=ORIENTED_EDGE('',*,*,#8290,.F.);
#11090=ORIENTED_EDGE('',*,*,#8298,.T.);
#11091=ORIENTED_EDGE('',*,*,#8294,.T.);
#11092=ORIENTED_EDGE('',*,*,#8295,.F.);
#11093=ORIENTED_EDGE('',*,*,#8298,.F.);
#11094=ORIENTED_EDGE('',*,*,#8289,.F.);
#11095=ORIENTED_EDGE('',*,*,#8265,.F.);
#11096=ORIENTED_EDGE('',*,*,#8299,.F.);
#11097=ORIENTED_EDGE('',*,*,#8156,.F.);
#11098=ORIENTED_EDGE('',*,*,#8297,.F.);
#11099=ORIENTED_EDGE('',*,*,#8268,.T.);
#11100=ORIENTED_EDGE('',*,*,#8300,.F.);
#11101=ORIENTED_EDGE('',*,*,#8301,.F.);
#11102=ORIENTED_EDGE('',*,*,#8302,.T.);
#11103=ORIENTED_EDGE('',*,*,#8267,.T.);
#11104=ORIENTED_EDGE('',*,*,#8276,.F.);
#11105=ORIENTED_EDGE('',*,*,#8303,.F.);
#11106=ORIENTED_EDGE('',*,*,#8300,.T.);
#11107=ORIENTED_EDGE('',*,*,#8269,.T.);
#11108=ORIENTED_EDGE('',*,*,#8302,.F.);
#11109=ORIENTED_EDGE('',*,*,#8304,.F.);
#11110=ORIENTED_EDGE('',*,*,#8283,.T.);
#11111=ORIENTED_EDGE('',*,*,#8301,.T.);
#11112=ORIENTED_EDGE('',*,*,#8303,.T.);
#11113=ORIENTED_EDGE('',*,*,#8275,.T.);
#11114=ORIENTED_EDGE('',*,*,#8305,.T.);
#11115=ORIENTED_EDGE('',*,*,#8306,.T.);
#11116=ORIENTED_EDGE('',*,*,#8284,.T.);
#11117=ORIENTED_EDGE('',*,*,#8304,.T.);
#11118=ORIENTED_EDGE('',*,*,#8274,.F.);
#11119=ORIENTED_EDGE('',*,*,#8307,.F.);
#11120=ORIENTED_EDGE('',*,*,#8308,.T.);
#11121=ORIENTED_EDGE('',*,*,#8309,.T.);
#11122=ORIENTED_EDGE('',*,*,#8310,.F.);
#11123=ORIENTED_EDGE('',*,*,#8311,.F.);
#11124=ORIENTED_EDGE('',*,*,#8309,.F.);
#11125=ORIENTED_EDGE('',*,*,#8312,.T.);
#11126=ORIENTED_EDGE('',*,*,#8313,.T.);
#11127=ORIENTED_EDGE('',*,*,#8314,.F.);
#11128=ORIENTED_EDGE('',*,*,#8313,.F.);
#11129=ORIENTED_EDGE('',*,*,#8315,.T.);
#11130=ORIENTED_EDGE('',*,*,#8316,.T.);
#11131=ORIENTED_EDGE('',*,*,#8317,.F.);
#11132=ORIENTED_EDGE('',*,*,#8318,.F.);
#11133=ORIENTED_EDGE('',*,*,#8316,.F.);
#11134=ORIENTED_EDGE('',*,*,#8319,.T.);
#11135=ORIENTED_EDGE('',*,*,#8320,.T.);
#11136=ORIENTED_EDGE('',*,*,#8321,.F.);
#11137=ORIENTED_EDGE('',*,*,#8320,.F.);
#11138=ORIENTED_EDGE('',*,*,#8322,.T.);
#11139=ORIENTED_EDGE('',*,*,#8286,.T.);
#11140=ORIENTED_EDGE('',*,*,#8262,.F.);
#11141=ORIENTED_EDGE('',*,*,#8288,.F.);
#11142=ORIENTED_EDGE('',*,*,#8323,.T.);
#11143=ORIENTED_EDGE('',*,*,#8324,.T.);
#11144=ORIENTED_EDGE('',*,*,#8263,.F.);
#11145=ORIENTED_EDGE('',*,*,#8324,.F.);
#11146=ORIENTED_EDGE('',*,*,#8325,.T.);
#11147=ORIENTED_EDGE('',*,*,#8326,.T.);
#11148=ORIENTED_EDGE('',*,*,#8264,.F.);
#11149=ORIENTED_EDGE('',*,*,#8326,.F.);
#11150=ORIENTED_EDGE('',*,*,#8327,.T.);
#11151=ORIENTED_EDGE('',*,*,#8328,.T.);
#11152=ORIENTED_EDGE('',*,*,#8329,.F.);
#11153=ORIENTED_EDGE('',*,*,#8330,.F.);
#11154=ORIENTED_EDGE('',*,*,#8328,.F.);
#11155=ORIENTED_EDGE('',*,*,#8331,.T.);
#11156=ORIENTED_EDGE('',*,*,#8332,.T.);
#11157=ORIENTED_EDGE('',*,*,#8333,.F.);
#11158=ORIENTED_EDGE('',*,*,#8332,.F.);
#11159=ORIENTED_EDGE('',*,*,#8334,.T.);
#11160=ORIENTED_EDGE('',*,*,#8335,.T.);
#11161=ORIENTED_EDGE('',*,*,#8157,.F.);
#11162=ORIENTED_EDGE('',*,*,#8151,.F.);
#11163=ORIENTED_EDGE('',*,*,#8336,.T.);
#11164=ORIENTED_EDGE('',*,*,#8337,.F.);
#11165=ORIENTED_EDGE('',*,*,#8158,.F.);
#11166=ORIENTED_EDGE('',*,*,#8335,.F.);
#11167=ORIENTED_EDGE('',*,*,#8338,.T.);
#11168=ORIENTED_EDGE('',*,*,#8339,.T.);
#11169=ORIENTED_EDGE('',*,*,#8138,.T.);
#11170=ORIENTED_EDGE('',*,*,#8340,.T.);
#11171=ORIENTED_EDGE('',*,*,#8341,.T.);
#11172=ORIENTED_EDGE('',*,*,#8342,.T.);
#11173=ORIENTED_EDGE('',*,*,#8293,.T.);
#11174=ORIENTED_EDGE('',*,*,#8343,.T.);
#11175=ORIENTED_EDGE('',*,*,#8344,.T.);
#11176=ORIENTED_EDGE('',*,*,#8155,.F.);
#11177=ORIENTED_EDGE('',*,*,#8144,.F.);
#11178=ORIENTED_EDGE('',*,*,#8345,.T.);
#11179=ORIENTED_EDGE('',*,*,#8346,.F.);
#11180=ORIENTED_EDGE('',*,*,#8336,.F.);
#11181=ORIENTED_EDGE('',*,*,#8347,.F.);
#11182=ORIENTED_EDGE('',*,*,#8348,.T.);
#11183=ORIENTED_EDGE('',*,*,#8341,.F.);
#11184=ORIENTED_EDGE('',*,*,#8349,.F.);
#11185=ORIENTED_EDGE('',*,*,#8149,.F.);
#11186=ORIENTED_EDGE('',*,*,#8305,.F.);
#11187=ORIENTED_EDGE('',*,*,#8310,.T.);
#11188=ORIENTED_EDGE('',*,*,#8311,.T.);
#11189=ORIENTED_EDGE('',*,*,#8314,.T.);
#11190=ORIENTED_EDGE('',*,*,#8350,.T.);
#11191=ORIENTED_EDGE('',*,*,#8141,.T.);
#11192=ORIENTED_EDGE('',*,*,#8351,.T.);
#11193=ORIENTED_EDGE('',*,*,#8352,.T.);
#11194=ORIENTED_EDGE('',*,*,#8353,.T.);
#11195=ORIENTED_EDGE('',*,*,#8291,.T.);
#11196=ORIENTED_EDGE('',*,*,#8337,.T.);
#11197=ORIENTED_EDGE('',*,*,#8346,.T.);
#11198=ORIENTED_EDGE('',*,*,#8354,.F.);
#11199=ORIENTED_EDGE('',*,*,#8355,.T.);
#11200=ORIENTED_EDGE('',*,*,#8307,.T.);
#11201=ORIENTED_EDGE('',*,*,#8273,.F.);
#11202=ORIENTED_EDGE('',*,*,#8342,.F.);
#11203=ORIENTED_EDGE('',*,*,#8348,.F.);
#11204=ORIENTED_EDGE('',*,*,#8355,.F.);
#11205=ORIENTED_EDGE('',*,*,#8356,.T.);
#11206=ORIENTED_EDGE('',*,*,#8357,.F.);
#11207=ORIENTED_EDGE('',*,*,#8358,.F.);
#11208=ORIENTED_EDGE('',*,*,#8359,.F.);
#11209=ORIENTED_EDGE('',*,*,#8152,.T.);
#11210=ORIENTED_EDGE('',*,*,#8338,.F.);
#11211=ORIENTED_EDGE('',*,*,#8334,.F.);
#11212=ORIENTED_EDGE('',*,*,#8331,.F.);
#11213=ORIENTED_EDGE('',*,*,#8327,.F.);
#11214=ORIENTED_EDGE('',*,*,#8325,.F.);
#11215=ORIENTED_EDGE('',*,*,#8323,.F.);
#11216=ORIENTED_EDGE('',*,*,#8287,.F.);
#11217=ORIENTED_EDGE('',*,*,#8322,.F.);
#11218=ORIENTED_EDGE('',*,*,#8319,.F.);
#11219=ORIENTED_EDGE('',*,*,#8315,.F.);
#11220=ORIENTED_EDGE('',*,*,#8312,.F.);
#11221=ORIENTED_EDGE('',*,*,#8308,.F.);
#11222=ORIENTED_EDGE('',*,*,#8213,.T.);
#11223=ORIENTED_EDGE('',*,*,#8216,.T.);
#11224=ORIENTED_EDGE('',*,*,#8208,.T.);
#11225=ORIENTED_EDGE('',*,*,#8202,.T.);
#11226=ORIENTED_EDGE('',*,*,#8196,.T.);
#11227=ORIENTED_EDGE('',*,*,#8193,.T.);
#11228=ORIENTED_EDGE('',*,*,#8201,.T.);
#11229=ORIENTED_EDGE('',*,*,#8207,.T.);
#11230=ORIENTED_EDGE('',*,*,#8134,.T.);
#11231=ORIENTED_EDGE('',*,*,#8142,.T.);
#11232=ORIENTED_EDGE('',*,*,#8350,.F.);
#11233=ORIENTED_EDGE('',*,*,#8345,.F.);
#11234=ORIENTED_EDGE('',*,*,#8150,.F.);
#11235=ORIENTED_EDGE('',*,*,#8349,.T.);
#11236=ORIENTED_EDGE('',*,*,#8340,.F.);
#11237=ORIENTED_EDGE('',*,*,#8140,.F.);
#11238=ORIENTED_EDGE('',*,*,#8306,.F.);
#11239=ORIENTED_EDGE('',*,*,#8317,.T.);
#11240=ORIENTED_EDGE('',*,*,#8318,.T.);
#11241=ORIENTED_EDGE('',*,*,#8321,.T.);
#11242=ORIENTED_EDGE('',*,*,#8285,.F.);
#11243=ORIENTED_EDGE('',*,*,#8147,.T.);
#11244=ORIENTED_EDGE('',*,*,#8220,.T.);
#11245=ORIENTED_EDGE('',*,*,#8139,.T.);
#11246=ORIENTED_EDGE('',*,*,#8339,.F.);
#11247=ORIENTED_EDGE('',*,*,#8360,.T.);
#11248=ORIENTED_EDGE('',*,*,#8361,.T.);
#11249=ORIENTED_EDGE('',*,*,#8362,.T.);
#11250=ORIENTED_EDGE('',*,*,#8360,.F.);
#11251=ORIENTED_EDGE('',*,*,#8344,.F.);
#11252=ORIENTED_EDGE('',*,*,#8363,.T.);
#11253=ORIENTED_EDGE('',*,*,#8154,.T.);
#11254=ORIENTED_EDGE('',*,*,#8364,.F.);
#11255=ORIENTED_EDGE('',*,*,#8352,.F.);
#11256=ORIENTED_EDGE('',*,*,#8364,.T.);
#11257=ORIENTED_EDGE('',*,*,#8153,.T.);
#11258=ORIENTED_EDGE('',*,*,#8359,.T.);
#11259=ORIENTED_EDGE('',*,*,#8365,.F.);
#11260=ORIENTED_EDGE('',*,*,#8366,.F.);
#11261=ORIENTED_EDGE('',*,*,#8353,.F.);
#11262=ORIENTED_EDGE('',*,*,#8333,.T.);
#11263=ORIENTED_EDGE('',*,*,#8299,.T.);
#11264=ORIENTED_EDGE('',*,*,#8329,.T.);
#11265=ORIENTED_EDGE('',*,*,#8330,.T.);
#11266=ORIENTED_EDGE('',*,*,#8357,.T.);
#11267=ORIENTED_EDGE('',*,*,#8367,.T.);
#11268=ORIENTED_EDGE('',*,*,#8361,.F.);
#11269=ORIENTED_EDGE('',*,*,#8343,.F.);
#11270=ORIENTED_EDGE('',*,*,#8368,.F.);
#11271=ORIENTED_EDGE('',*,*,#8369,.T.);
#11272=ORIENTED_EDGE('',*,*,#8292,.T.);
#11273=ORIENTED_EDGE('',*,*,#8366,.T.);
#11274=ORIENTED_EDGE('',*,*,#8370,.T.);
#11275=ORIENTED_EDGE('',*,*,#8368,.T.);
#11276=ORIENTED_EDGE('',*,*,#8358,.T.);
#11277=ORIENTED_EDGE('',*,*,#8369,.F.);
#11278=ORIENTED_EDGE('',*,*,#8370,.F.);
#11279=ORIENTED_EDGE('',*,*,#8365,.T.);
#11280=ORIENTED_EDGE('',*,*,#8371,.T.);
#11281=ORIENTED_EDGE('',*,*,#8198,.T.);
#11282=ORIENTED_EDGE('',*,*,#8372,.F.);
#11283=ORIENTED_EDGE('',*,*,#8373,.F.);
#11284=ORIENTED_EDGE('',*,*,#8372,.T.);
#11285=ORIENTED_EDGE('',*,*,#8204,.T.);
#11286=ORIENTED_EDGE('',*,*,#8374,.F.);
#11287=ORIENTED_EDGE('',*,*,#8375,.F.);
#11288=ORIENTED_EDGE('',*,*,#8374,.T.);
#11289=ORIENTED_EDGE('',*,*,#8210,.T.);
#11290=ORIENTED_EDGE('',*,*,#8376,.F.);
#11291=ORIENTED_EDGE('',*,*,#8377,.F.);
#11292=ORIENTED_EDGE('',*,*,#8376,.T.);
#11293=ORIENTED_EDGE('',*,*,#8217,.T.);
#11294=ORIENTED_EDGE('',*,*,#8378,.F.);
#11295=ORIENTED_EDGE('',*,*,#8379,.F.);
#11296=ORIENTED_EDGE('',*,*,#8378,.T.);
#11297=ORIENTED_EDGE('',*,*,#8211,.T.);
#11298=ORIENTED_EDGE('',*,*,#8380,.F.);
#11299=ORIENTED_EDGE('',*,*,#8381,.F.);
#11300=ORIENTED_EDGE('',*,*,#8380,.T.);
#11301=ORIENTED_EDGE('',*,*,#8205,.T.);
#11302=ORIENTED_EDGE('',*,*,#8382,.F.);
#11303=ORIENTED_EDGE('',*,*,#8383,.F.);
#11304=ORIENTED_EDGE('',*,*,#8384,.T.);
#11305=ORIENTED_EDGE('',*,*,#8195,.T.);
#11306=ORIENTED_EDGE('',*,*,#8371,.F.);
#11307=ORIENTED_EDGE('',*,*,#8385,.F.);
#11308=ORIENTED_EDGE('',*,*,#8347,.T.);
#11309=ORIENTED_EDGE('',*,*,#8148,.T.);
#11310=ORIENTED_EDGE('',*,*,#8362,.F.);
#11311=ORIENTED_EDGE('',*,*,#8367,.F.);
#11312=ORIENTED_EDGE('',*,*,#8356,.F.);
#11313=ORIENTED_EDGE('',*,*,#8354,.T.);
#11314=ORIENTED_EDGE('',*,*,#8123,.F.);
#11315=ORIENTED_EDGE('',*,*,#8146,.T.);
#11316=ORIENTED_EDGE('',*,*,#8363,.F.);
#11317=ORIENTED_EDGE('',*,*,#8351,.F.);
#11318=ORIENTED_EDGE('',*,*,#8143,.F.);
#11319=ORIENTED_EDGE('',*,*,#8382,.T.);
#11320=ORIENTED_EDGE('',*,*,#8199,.T.);
#11321=ORIENTED_EDGE('',*,*,#8384,.F.);
#11322=ORIENTED_EDGE('',*,*,#8386,.F.);
#11323=ORIENTED_EDGE('',*,*,#8119,.F.);
#11324=ORIENTED_EDGE('',*,*,#8112,.T.);
#11325=ORIENTED_EDGE('',*,*,#8115,.T.);
#11326=ORIENTED_EDGE('',*,*,#8387,.F.);
#11327=ORIENTED_EDGE('',*,*,#8109,.F.);
#11328=ORIENTED_EDGE('',*,*,#8191,.F.);
#11329=ORIENTED_EDGE('',*,*,#8101,.T.);
#11330=ORIENTED_EDGE('',*,*,#8388,.F.);
#11331=ORIENTED_EDGE('',*,*,#8214,.F.);
#11332=ORIENTED_EDGE('',*,*,#8188,.T.);
#11333=ORIENTED_EDGE('',*,*,#8389,.F.);
#11334=ORIENTED_EDGE('',*,*,#8186,.T.);
#11335=ORIENTED_EDGE('',*,*,#8171,.T.);
#11336=ORIENTED_EDGE('',*,*,#8390,.T.);
#11337=ORIENTED_EDGE('',*,*,#8389,.T.);
#11338=ORIENTED_EDGE('',*,*,#8190,.T.);
#11339=ORIENTED_EDGE('',*,*,#8175,.T.);
#11340=ORIENTED_EDGE('',*,*,#8187,.T.);
#11341=ORIENTED_EDGE('',*,*,#8391,.F.);
#11342=ORIENTED_EDGE('',*,*,#8392,.T.);
#11343=ORIENTED_EDGE('',*,*,#8393,.T.);
#11344=ORIENTED_EDGE('',*,*,#8394,.T.);
#11345=ORIENTED_EDGE('',*,*,#8395,.F.);
#11346=ORIENTED_EDGE('',*,*,#8396,.T.);
#11347=ORIENTED_EDGE('',*,*,#8397,.T.);
#11348=ORIENTED_EDGE('',*,*,#8398,.T.);
#11349=ORIENTED_EDGE('',*,*,#8399,.F.);
#11350=ORIENTED_EDGE('',*,*,#8400,.T.);
#11351=ORIENTED_EDGE('',*,*,#8395,.T.);
#11352=ORIENTED_EDGE('',*,*,#8401,.T.);
#11353=ORIENTED_EDGE('',*,*,#8393,.F.);
#11354=ORIENTED_EDGE('',*,*,#8402,.T.);
#11355=ORIENTED_EDGE('',*,*,#8403,.F.);
#11356=ORIENTED_EDGE('',*,*,#8396,.F.);
#11357=ORIENTED_EDGE('',*,*,#8400,.F.);
#11358=ORIENTED_EDGE('',*,*,#8404,.F.);
#11359=ORIENTED_EDGE('',*,*,#8405,.T.);
#11360=ORIENTED_EDGE('',*,*,#8404,.T.);
#11361=ORIENTED_EDGE('',*,*,#8399,.T.);
#11362=ORIENTED_EDGE('',*,*,#8406,.T.);
#11363=ORIENTED_EDGE('',*,*,#8397,.F.);
#11364=ORIENTED_EDGE('',*,*,#8403,.T.);
#11365=ORIENTED_EDGE('',*,*,#8405,.F.);
#11366=ORIENTED_EDGE('',*,*,#8407,.T.);
#11367=ORIENTED_EDGE('',*,*,#8391,.T.);
#11368=ORIENTED_EDGE('',*,*,#8408,.T.);
#11369=ORIENTED_EDGE('',*,*,#8409,.F.);
#11370=ORIENTED_EDGE('',*,*,#8182,.T.);
#11371=ORIENTED_EDGE('',*,*,#8162,.T.);
#11372=ORIENTED_EDGE('',*,*,#8410,.T.);
#11373=ORIENTED_EDGE('',*,*,#8185,.F.);
#11374=ORIENTED_EDGE('',*,*,#8183,.T.);
#11375=ORIENTED_EDGE('',*,*,#8409,.T.);
#11376=ORIENTED_EDGE('',*,*,#8411,.T.);
#11377=ORIENTED_EDGE('',*,*,#8169,.F.);
#11378=ORIENTED_EDGE('',*,*,#8180,.T.);
#11379=ORIENTED_EDGE('',*,*,#8402,.F.);
#11380=ORIENTED_EDGE('',*,*,#8392,.F.);
#11381=ORIENTED_EDGE('',*,*,#8407,.F.);
#11382=ORIENTED_EDGE('',*,*,#8406,.F.);
#11383=ORIENTED_EDGE('',*,*,#8104,.F.);
#11384=ORIENTED_EDGE('',*,*,#8107,.F.);
#11385=ORIENTED_EDGE('',*,*,#8387,.T.);
#11386=ORIENTED_EDGE('',*,*,#8114,.T.);
#11387=ORIENTED_EDGE('',*,*,#8218,.T.);
#11388=ORIENTED_EDGE('',*,*,#8117,.T.);
#11389=ORIENTED_EDGE('',*,*,#8386,.T.);
#11390=ORIENTED_EDGE('',*,*,#8385,.T.);
#11391=ORIENTED_EDGE('',*,*,#8373,.T.);
#11392=ORIENTED_EDGE('',*,*,#8375,.T.);
#11393=ORIENTED_EDGE('',*,*,#8377,.T.);
#11394=ORIENTED_EDGE('',*,*,#8379,.T.);
#11395=ORIENTED_EDGE('',*,*,#8381,.T.);
#11396=ORIENTED_EDGE('',*,*,#8383,.T.);
#11397=ORIENTED_EDGE('',*,*,#8388,.T.);
#11398=ORIENTED_EDGE('',*,*,#8100,.F.);
#11399=ORIENTED_EDGE('',*,*,#8411,.F.);
#11400=ORIENTED_EDGE('',*,*,#8410,.F.);
#11401=ORIENTED_EDGE('',*,*,#8167,.F.);
#11402=ORIENTED_EDGE('',*,*,#8170,.F.);
#11403=ORIENTED_EDGE('',*,*,#8178,.F.);
#11404=ORIENTED_EDGE('',*,*,#8215,.F.);
#11405=ORIENTED_EDGE('',*,*,#8390,.F.);
#11406=ORIENTED_EDGE('',*,*,#8174,.F.);
#11407=ORIENTED_EDGE('',*,*,#8408,.F.);
#11408=ORIENTED_EDGE('',*,*,#8394,.F.);
#11409=ORIENTED_EDGE('',*,*,#8401,.F.);
#11410=ORIENTED_EDGE('',*,*,#8398,.F.);
#14514=ADVANCED_FACE('',(#3879),#3464,.T.);
#14515=ADVANCED_FACE('',(#3880),#3465,.F.);
#14516=ADVANCED_FACE('',(#3881),#3466,.F.);
#14517=ADVANCED_FACE('',(#3882),#3467,.F.);
#14518=ADVANCED_FACE('',(#3883),#3468,.T.);
#14519=ADVANCED_FACE('',(#3884),#431,.F.);
#14520=ADVANCED_FACE('',(#3885),#432,.F.);
#14521=ADVANCED_FACE('',(#3886),#433,.F.);
#14522=ADVANCED_FACE('',(#3887),#434,.F.);
#14523=ADVANCED_FACE('',(#3888),#435,.T.);
#14524=ADVANCED_FACE('',(#3889),#436,.T.);
#14525=ADVANCED_FACE('',(#3890),#437,.F.);
#14526=ADVANCED_FACE('',(#3891),#438,.F.);
#14527=ADVANCED_FACE('',(#3892),#439,.F.);
#14528=ADVANCED_FACE('',(#3893),#440,.F.);
#14529=ADVANCED_FACE('',(#3894),#441,.T.);
#14530=ADVANCED_FACE('',(#3895),#442,.T.);
#14531=ADVANCED_FACE('',(#3896),#443,.F.);
#14532=ADVANCED_FACE('',(#3897),#444,.F.);
#14533=ADVANCED_FACE('',(#3898),#445,.T.);
#14534=ADVANCED_FACE('',(#3899),#446,.F.);
#14535=ADVANCED_FACE('',(#3900),#447,.F.);
#14536=ADVANCED_FACE('',(#3901),#448,.F.);
#14537=ADVANCED_FACE('',(#3902),#449,.F.);
#14538=ADVANCED_FACE('',(#3903),#450,.T.);
#14539=ADVANCED_FACE('',(#3904),#451,.T.);
#14540=ADVANCED_FACE('',(#3905),#452,.T.);
#14541=ADVANCED_FACE('',(#3906),#453,.T.);
#14542=ADVANCED_FACE('',(#3907),#454,.T.);
#14543=ADVANCED_FACE('',(#3908),#455,.T.);
#14544=ADVANCED_FACE('',(#3909),#1037,.F.);
#14545=ADVANCED_FACE('',(#3910),#456,.F.);
#14546=ADVANCED_FACE('',(#3911),#457,.F.);
#14547=ADVANCED_FACE('',(#3912),#1038,.F.);
#14548=ADVANCED_FACE('',(#3913),#1039,.F.);
#14549=ADVANCED_FACE('',(#3914),#458,.F.);
#14550=ADVANCED_FACE('',(#3915),#459,.F.);
#14551=ADVANCED_FACE('',(#3916),#460,.F.);
#14552=ADVANCED_FACE('',(#3917),#1040,.F.);
#14553=ADVANCED_FACE('',(#3918),#461,.T.);
#14554=ADVANCED_FACE('',(#3919),#462,.T.);
#14555=ADVANCED_FACE('',(#3920),#463,.T.);
#14556=ADVANCED_FACE('',(#3921),#464,.F.);
#14557=ADVANCED_FACE('',(#3922),#465,.T.);
#14558=ADVANCED_FACE('',(#3923),#466,.T.);
#14559=ADVANCED_FACE('',(#3924),#3469,.T.);
#14560=ADVANCED_FACE('',(#3925),#467,.T.);
#14561=ADVANCED_FACE('',(#3926),#3470,.T.);
#14562=ADVANCED_FACE('',(#3927),#3471,.T.);
#14563=ADVANCED_FACE('',(#3928),#468,.T.);
#14564=ADVANCED_FACE('',(#3929),#3472,.T.);
#14565=ADVANCED_FACE('',(#3930),#3473,.T.);
#14566=ADVANCED_FACE('',(#3931),#469,.T.);
#14567=ADVANCED_FACE('',(#3932),#3474,.T.);
#14568=ADVANCED_FACE('',(#3933),#3475,.T.);
#14569=ADVANCED_FACE('',(#3934),#470,.F.);
#14570=ADVANCED_FACE('',(#3935,#217),#471,.T.);
#14571=ADVANCED_FACE('',(#3936,#218),#472,.T.);
#14572=ADVANCED_FACE('',(#3937),#473,.T.);
#14573=ADVANCED_FACE('',(#3938),#474,.T.);
#14574=ADVANCED_FACE('',(#3939,#219),#475,.F.);
#14575=ADVANCED_FACE('',(#3940),#476,.T.);
#14576=ADVANCED_FACE('',(#3941),#477,.T.);
#14577=ADVANCED_FACE('',(#3942),#478,.T.);
#14578=ADVANCED_FACE('',(#3943),#479,.T.);
#14579=ADVANCED_FACE('',(#3944),#480,.T.);
#14580=ADVANCED_FACE('',(#3945),#481,.F.);
#14581=ADVANCED_FACE('',(#3946),#482,.T.);
#14582=ADVANCED_FACE('',(#3947),#483,.T.);
#14583=ADVANCED_FACE('',(#3948),#484,.T.);
#14584=ADVANCED_FACE('',(#3949),#485,.F.);
#14585=ADVANCED_FACE('',(#3950),#486,.F.);
#14586=ADVANCED_FACE('',(#3951),#487,.F.);
#14587=ADVANCED_FACE('',(#3952),#488,.F.);
#14588=ADVANCED_FACE('',(#3953),#489,.T.);
#14589=ADVANCED_FACE('',(#3954),#490,.T.);
#14590=ADVANCED_FACE('',(#3955),#491,.T.);
#14591=ADVANCED_FACE('',(#3956),#492,.T.);
#14592=ADVANCED_FACE('',(#3957),#493,.T.);
#14593=ADVANCED_FACE('',(#3958),#3476,.T.);
#14594=ADVANCED_FACE('',(#3959),#3477,.T.);
#14595=ADVANCED_FACE('',(#3960),#494,.T.);
#14596=ADVANCED_FACE('',(#3961),#495,.T.);
#14597=ADVANCED_FACE('',(#3962),#496,.T.);
#14598=ADVANCED_FACE('',(#3963),#497,.T.);
#14599=ADVANCED_FACE('',(#3964),#498,.T.);
#14600=ADVANCED_FACE('',(#3965),#499,.T.);
#14601=ADVANCED_FACE('',(#3966),#3478,.T.);
#14602=ADVANCED_FACE('',(#3967),#3479,.T.);
#14603=ADVANCED_FACE('',(#3968),#500,.T.);
#14604=ADVANCED_FACE('',(#3969),#501,.T.);
#14605=ADVANCED_FACE('',(#3970),#502,.T.);
#14606=ADVANCED_FACE('',(#3971,#220),#503,.F.);
#14607=ADVANCED_FACE('',(#3972),#504,.T.);
#14608=ADVANCED_FACE('',(#3973),#505,.T.);
#14609=ADVANCED_FACE('',(#3974),#506,.F.);
#14610=ADVANCED_FACE('',(#3975),#3480,.F.);
#14611=ADVANCED_FACE('',(#3976),#3481,.F.);
#14612=ADVANCED_FACE('',(#3977),#507,.F.);
#14613=ADVANCED_FACE('',(#3978),#508,.T.);
#14614=ADVANCED_FACE('',(#3979),#509,.F.);
#14615=ADVANCED_FACE('',(#3980),#510,.T.);
#14616=ADVANCED_FACE('',(#3981),#511,.F.);
#14617=ADVANCED_FACE('',(#3982),#512,.F.);
#14618=ADVANCED_FACE('',(#3983),#3482,.F.);
#14619=ADVANCED_FACE('',(#3984),#513,.F.);
#14620=ADVANCED_FACE('',(#3985),#3483,.F.);
#14621=ADVANCED_FACE('',(#3986),#514,.F.);
#14622=ADVANCED_FACE('',(#3987),#3484,.F.);
#14623=ADVANCED_FACE('',(#3988),#3485,.F.);
#14624=ADVANCED_FACE('',(#3989),#515,.F.);
#14625=ADVANCED_FACE('',(#3990),#516,.F.);
#14626=ADVANCED_FACE('',(#3991),#517,.F.);
#14627=ADVANCED_FACE('',(#3992),#518,.F.);
#14628=ADVANCED_FACE('',(#3993),#519,.T.);
#14629=ADVANCED_FACE('',(#3994),#520,.F.);
#14630=ADVANCED_FACE('',(#3995),#521,.F.);
#14631=ADVANCED_FACE('',(#3996),#522,.F.);
#14632=ADVANCED_FACE('',(#3997),#523,.T.);
#14633=ADVANCED_FACE('',(#3998),#524,.T.);
#14634=ADVANCED_FACE('',(#3999),#525,.F.);
#14635=ADVANCED_FACE('',(#4000),#526,.F.);
#14636=ADVANCED_FACE('',(#4001),#527,.F.);
#14637=ADVANCED_FACE('',(#4002),#528,.T.);
#14638=ADVANCED_FACE('',(#4003,#221,#222,#223),#529,.T.);
#15195=CLOSED_SHELL('',(#14514,#14515,#14516,#14517,#14518,#14519,#14520,
#14521,#14522,#14523,#14524,#14525,#14526,#14527,#14528,#14529,#14530,#14531,
#14532,#14533,#14534,#14535,#14536,#14537,#14538,#14539,#14540,#14541,#14542,
#14543,#14544,#14545,#14546,#14547,#14548,#14549,#14550,#14551,#14552,#14553,
#14554,#14555,#14556,#14557,#14558,#14559,#14560,#14561,#14562,#14563,#14564,
#14565,#14566,#14567,#14568,#14569,#14570,#14571,#14572,#14573,#14574,#14575,
#14576,#14577,#14578,#14579,#14580,#14581,#14582,#14583,#14584,#14585,#14586,
#14587,#14588,#14589,#14590,#14591,#14592,#14593,#14594,#14595,#14596,#14597,
#14598,#14599,#14600,#14601,#14602,#14603,#14604,#14605,#14606,#14607,#14608,
#14609,#14610,#14611,#14612,#14613,#14614,#14615,#14616,#14617,#14618,#14619,
#14620,#14621,#14622,#14623,#14624,#14625,#14626,#14627,#14628,#14629,#14630,
#14631,#14632,#14633,#14634,#14635,#14636,#14637,#14638));
#15679=AXIS2_PLACEMENT_3D('',#34475,#17938,#17939);
#15680=AXIS2_PLACEMENT_3D('',#34476,#17940,#17941);
#15681=AXIS2_PLACEMENT_3D('',#34479,#17942,#17943);
#15682=AXIS2_PLACEMENT_3D('',#34481,#17944,#17945);
#15683=AXIS2_PLACEMENT_3D('',#34483,#17946,#17947);
#15684=AXIS2_PLACEMENT_3D('',#34487,#17949,#17950);
#15685=AXIS2_PLACEMENT_3D('',#34489,#17952,#17953);
#15686=AXIS2_PLACEMENT_3D('',#34491,#17954,#17955);
#15687=AXIS2_PLACEMENT_3D('',#34494,#17957,#17958);
#15688=AXIS2_PLACEMENT_3D('',#34495,#17959,#17960);
#15689=AXIS2_PLACEMENT_3D('',#34498,#17961,#17962);
#15690=AXIS2_PLACEMENT_3D('',#34502,#17964,#17965);
#15691=AXIS2_PLACEMENT_3D('',#34504,#17967,#17968);
#15692=AXIS2_PLACEMENT_3D('',#34507,#17969,#17970);
#15693=AXIS2_PLACEMENT_3D('',#34511,#17972,#17973);
#15694=AXIS2_PLACEMENT_3D('',#34513,#17975,#17976);
#15695=AXIS2_PLACEMENT_3D('',#34516,#17977,#17978);
#15696=AXIS2_PLACEMENT_3D('',#34520,#17980,#17981);
#15697=AXIS2_PLACEMENT_3D('',#34522,#17982,#17983);
#15698=AXIS2_PLACEMENT_3D('',#34524,#17985,#17986);
#15699=AXIS2_PLACEMENT_3D('',#34533,#17991,#17992);
#15700=AXIS2_PLACEMENT_3D('',#34539,#17996,#17997);
#15701=AXIS2_PLACEMENT_3D('',#34545,#18001,#18002);
#15702=AXIS2_PLACEMENT_3D('',#34554,#18007,#18008);
#15703=AXIS2_PLACEMENT_3D('',#34560,#18012,#18013);
#15704=AXIS2_PLACEMENT_3D('',#34566,#18017,#18018);
#15705=AXIS2_PLACEMENT_3D('',#34575,#18023,#18024);
#15706=AXIS2_PLACEMENT_3D('',#34584,#18029,#18030);
#15707=AXIS2_PLACEMENT_3D('',#34591,#18035,#18036);
#15708=AXIS2_PLACEMENT_3D('',#34602,#18043,#18044);
#15709=AXIS2_PLACEMENT_3D('',#34608,#18048,#18049);
#15710=AXIS2_PLACEMENT_3D('',#34614,#18053,#18054);
#15711=AXIS2_PLACEMENT_3D('',#34617,#18055,#18056);
#15712=AXIS2_PLACEMENT_3D('',#34626,#18061,#18062);
#15713=AXIS2_PLACEMENT_3D('',#34628,#18064,#18065);
#15714=AXIS2_PLACEMENT_3D('',#34636,#18069,#18070);
#15715=AXIS2_PLACEMENT_3D('',#34637,#18071,#18072);
#15716=AXIS2_PLACEMENT_3D('',#34638,#18073,#18074);
#15717=AXIS2_PLACEMENT_3D('',#34651,#18081,#18082);
#15718=AXIS2_PLACEMENT_3D('',#34664,#18089,#18090);
#15719=AXIS2_PLACEMENT_3D('',#34670,#18094,#18095);
#15720=AXIS2_PLACEMENT_3D('',#34679,#18100,#18101);
#15721=AXIS2_PLACEMENT_3D('',#34689,#18107,#18108);
#15722=AXIS2_PLACEMENT_3D('',#34693,#18111,#18112);
#15723=AXIS2_PLACEMENT_3D('',#34699,#18116,#18117);
#15724=AXIS2_PLACEMENT_3D('',#34701,#18119,#18120);
#15725=AXIS2_PLACEMENT_3D('',#34705,#18123,#18124);
#15726=AXIS2_PLACEMENT_3D('',#34711,#18128,#18129);
#15727=AXIS2_PLACEMENT_3D('',#34713,#18131,#18132);
#15728=AXIS2_PLACEMENT_3D('',#34718,#18134,#18135);
#15729=AXIS2_PLACEMENT_3D('',#34721,#18137,#18138);
#15730=AXIS2_PLACEMENT_3D('',#34722,#18139,#18140);
#15731=AXIS2_PLACEMENT_3D('',#34728,#18144,#18145);
#15732=AXIS2_PLACEMENT_3D('',#34734,#18149,#18150);
#15733=AXIS2_PLACEMENT_3D('',#34736,#18151,#18152);
#15734=AXIS2_PLACEMENT_3D('',#34739,#18154,#18155);
#15735=AXIS2_PLACEMENT_3D('',#34740,#18156,#18157);
#15736=AXIS2_PLACEMENT_3D('',#34742,#18158,#18159);
#15737=AXIS2_PLACEMENT_3D('',#34745,#18161,#18162);
#15738=AXIS2_PLACEMENT_3D('',#34746,#18163,#18164);
#15739=AXIS2_PLACEMENT_3D('',#34752,#18168,#18169);
#15740=AXIS2_PLACEMENT_3D('',#34758,#18173,#18174);
#15741=AXIS2_PLACEMENT_3D('',#34762,#18177,#18178);
#15742=AXIS2_PLACEMENT_3D('',#34763,#18179,#18180);
#15743=AXIS2_PLACEMENT_3D('',#34764,#18181,#18182);
#15744=AXIS2_PLACEMENT_3D('',#34765,#18183,#18184);
#15745=AXIS2_PLACEMENT_3D('',#34767,#18186,#18187);
#15746=AXIS2_PLACEMENT_3D('',#34770,#18190,#18191);
#15747=AXIS2_PLACEMENT_3D('',#34771,#18192,#18193);
#15748=AXIS2_PLACEMENT_3D('',#34772,#18194,#18195);
#15749=AXIS2_PLACEMENT_3D('',#34780,#18201,#18202);
#15750=AXIS2_PLACEMENT_3D('',#34786,#18206,#18207);
#15751=AXIS2_PLACEMENT_3D('',#34788,#18208,#18209);
#15752=AXIS2_PLACEMENT_3D('',#34790,#18210,#18211);
#15753=AXIS2_PLACEMENT_3D('',#34792,#18213,#18214);
#15754=AXIS2_PLACEMENT_3D('',#34800,#18219,#18220);
#15755=AXIS2_PLACEMENT_3D('',#34802,#18221,#18222);
#15756=AXIS2_PLACEMENT_3D('',#34804,#18223,#18224);
#15757=AXIS2_PLACEMENT_3D('',#34806,#18226,#18227);
#15758=AXIS2_PLACEMENT_3D('',#34808,#18228,#18229);
#15759=AXIS2_PLACEMENT_3D('',#34811,#18231,#18232);
#15760=AXIS2_PLACEMENT_3D('',#34812,#18233,#18234);
#15761=AXIS2_PLACEMENT_3D('',#34815,#18237,#18238);
#15762=AXIS2_PLACEMENT_3D('',#34817,#18239,#18240);
#15763=AXIS2_PLACEMENT_3D('',#34820,#18242,#18243);
#15764=AXIS2_PLACEMENT_3D('',#34821,#18244,#18245);
#15765=AXIS2_PLACEMENT_3D('',#34823,#18246,#18247);
#15766=AXIS2_PLACEMENT_3D('',#34825,#18248,#18249);
#15767=AXIS2_PLACEMENT_3D('',#34827,#18251,#18252);
#15768=AXIS2_PLACEMENT_3D('',#34833,#18256,#18257);
#15769=AXIS2_PLACEMENT_3D('',#34834,#18258,#18259);
#15770=AXIS2_PLACEMENT_3D('',#34835,#18260,#18261);
#15771=AXIS2_PLACEMENT_3D('',#34836,#18262,#18263);
#15772=AXIS2_PLACEMENT_3D('',#34838,#18264,#18265);
#15773=AXIS2_PLACEMENT_3D('',#34840,#18266,#18267);
#15774=AXIS2_PLACEMENT_3D('',#34842,#18269,#18270);
#15775=AXIS2_PLACEMENT_3D('',#34844,#18272,#18273);
#15776=AXIS2_PLACEMENT_3D('',#34846,#18275,#18276);
#15777=AXIS2_PLACEMENT_3D('',#34848,#18278,#18279);
#15778=AXIS2_PLACEMENT_3D('',#34849,#18280,#18281);
#15779=AXIS2_PLACEMENT_3D('',#34854,#18283,#18284);
#15780=AXIS2_PLACEMENT_3D('',#34860,#18288,#18289);
#15781=AXIS2_PLACEMENT_3D('',#34862,#18291,#18292);
#15782=AXIS2_PLACEMENT_3D('',#34874,#18299,#18300);
#15783=AXIS2_PLACEMENT_3D('',#34875,#18301,#18302);
#15784=AXIS2_PLACEMENT_3D('',#34885,#18308,#18309);
#15785=AXIS2_PLACEMENT_3D('',#34894,#18315,#18316);
#15786=AXIS2_PLACEMENT_3D('',#34909,#18325,#18326);
#15787=AXIS2_PLACEMENT_3D('',#34915,#18330,#18331);
#15788=AXIS2_PLACEMENT_3D('',#34921,#18335,#18336);
#15789=AXIS2_PLACEMENT_3D('',#34923,#18338,#18339);
#15790=AXIS2_PLACEMENT_3D('',#34925,#18341,#18342);
#15791=AXIS2_PLACEMENT_3D('',#34927,#18344,#18345);
#15792=AXIS2_PLACEMENT_3D('',#34933,#18349,#18350);
#15793=AXIS2_PLACEMENT_3D('',#34935,#18352,#18353);
#15794=AXIS2_PLACEMENT_3D('',#34937,#18355,#18356);
#15795=AXIS2_PLACEMENT_3D('',#34941,#18359,#18360);
#15796=AXIS2_PLACEMENT_3D('',#34949,#18365,#18366);
#15797=AXIS2_PLACEMENT_3D('',#34955,#18370,#18371);
#15798=AXIS2_PLACEMENT_3D('',#34962,#18376,#18377);
#15799=AXIS2_PLACEMENT_3D('',#34968,#18381,#18382);
#15800=AXIS2_PLACEMENT_3D('',#34969,#18383,#18384);
#15801=AXIS2_PLACEMENT_3D('',#34970,#18385,#18386);
#15802=AXIS2_PLACEMENT_3D('',#34971,#18387,#18388);
#15803=AXIS2_PLACEMENT_3D('',#34973,#18389,#18390);
#15804=AXIS2_PLACEMENT_3D('',#34975,#18392,#18393);
#15805=AXIS2_PLACEMENT_3D('',#34979,#18396,#18397);
#15806=AXIS2_PLACEMENT_3D('',#34985,#18401,#18402);
#15807=AXIS2_PLACEMENT_3D('',#34991,#18406,#18407);
#15808=AXIS2_PLACEMENT_3D('',#34996,#18411,#18412);
#15809=AXIS2_PLACEMENT_3D('',#35001,#18416,#18417);
#15810=AXIS2_PLACEMENT_3D('',#35007,#18420,#18421);
#15811=AXIS2_PLACEMENT_3D('',#35011,#18424,#18425);
#15812=AXIS2_PLACEMENT_3D('',#35012,#18426,#18427);
#15813=AXIS2_PLACEMENT_3D('',#35015,#18429,#18430);
#15814=AXIS2_PLACEMENT_3D('',#35016,#18431,#18432);
#15815=AXIS2_PLACEMENT_3D('',#35018,#18433,#18434);
#15816=AXIS2_PLACEMENT_3D('',#35021,#18437,#18438);
#15817=AXIS2_PLACEMENT_3D('',#35022,#18439,#18440);
#15818=AXIS2_PLACEMENT_3D('',#35027,#18443,#18444);
#15819=AXIS2_PLACEMENT_3D('',#35029,#18446,#18447);
#15820=AXIS2_PLACEMENT_3D('',#35033,#18450,#18451);
#15821=AXIS2_PLACEMENT_3D('',#35041,#18456,#18457);
#15822=AXIS2_PLACEMENT_3D('',#35042,#18458,#18459);
#15823=AXIS2_PLACEMENT_3D('',#35043,#18460,#18461);
#15824=AXIS2_PLACEMENT_3D('',#35045,#18463,#18464);
#15825=AXIS2_PLACEMENT_3D('',#35048,#18466,#18467);
#15826=AXIS2_PLACEMENT_3D('',#35049,#18468,#18469);
#15827=AXIS2_PLACEMENT_3D('',#35052,#18472,#18473);
#15828=AXIS2_PLACEMENT_3D('',#35056,#18476,#18477);
#15829=AXIS2_PLACEMENT_3D('',#35057,#18478,#18479);
#15830=AXIS2_PLACEMENT_3D('',#35062,#18483,#18484);
#15831=AXIS2_PLACEMENT_3D('',#35064,#18486,#18487);
#15832=AXIS2_PLACEMENT_3D('',#35065,#18488,#18489);
#15833=AXIS2_PLACEMENT_3D('',#35071,#18493,#18494);
#15834=AXIS2_PLACEMENT_3D('',#35074,#18496,#18497);
#15835=AXIS2_PLACEMENT_3D('',#35075,#18498,#18499);
#15836=AXIS2_PLACEMENT_3D('',#35079,#18502,#18503);
#15837=AXIS2_PLACEMENT_3D('',#35082,#18505,#18506);
#15838=AXIS2_PLACEMENT_3D('',#35083,#18507,#18508);
#15839=AXIS2_PLACEMENT_3D('',#35087,#18511,#18512);
#15840=AXIS2_PLACEMENT_3D('',#35090,#18514,#18515);
#15841=AXIS2_PLACEMENT_3D('',#35091,#18516,#18517);
#15842=AXIS2_PLACEMENT_3D('',#35094,#18519,#18520);
#15843=AXIS2_PLACEMENT_3D('',#35095,#18521,#18522);
#15844=AXIS2_PLACEMENT_3D('',#35096,#18523,#18524);
#15845=AXIS2_PLACEMENT_3D('',#35097,#18525,#18526);
#15846=AXIS2_PLACEMENT_3D('',#35101,#18530,#18531);
#15847=AXIS2_PLACEMENT_3D('',#35104,#18534,#18535);
#15848=AXIS2_PLACEMENT_3D('',#35105,#18536,#18537);
#15849=AXIS2_PLACEMENT_3D('',#35114,#18542,#18543);
#15850=AXIS2_PLACEMENT_3D('',#35123,#18548,#18549);
#15851=AXIS2_PLACEMENT_3D('',#35130,#18554,#18555);
#15852=AXIS2_PLACEMENT_3D('',#35134,#18558,#18559);
#15853=AXIS2_PLACEMENT_3D('',#35138,#18562,#18563);
#15854=AXIS2_PLACEMENT_3D('',#35141,#18566,#18567);
#15855=AXIS2_PLACEMENT_3D('',#35145,#18570,#18571);
#15856=AXIS2_PLACEMENT_3D('',#35147,#18573,#18574);
#15857=AXIS2_PLACEMENT_3D('',#35148,#18575,#18576);
#17938=DIRECTION('axis',(0.,0.,1.));
#17939=DIRECTION('refdir',(1.,0.,0.));
#17940=DIRECTION('center_axis',(1.,0.,0.));
#17941=DIRECTION('ref_axis',(0.,0.393919298579167,0.919145030018058));
#17942=DIRECTION('center_axis',(-1.,0.,0.));
#17943=DIRECTION('ref_axis',(0.,0.906392585430544,-0.422436363345457));
#17944=DIRECTION('center_axis',(-1.,0.,0.));
#17945=DIRECTION('ref_axis',(0.,0.906392585430544,-0.422436363345457));
#17946=DIRECTION('center_axis',(-1.,0.,0.));
#17947=DIRECTION('ref_axis',(0.,0.906392585430544,-0.422436363345457));
#17948=DIRECTION('',(-1.,0.,0.));
#17949=DIRECTION('center_axis',(-1.,0.,0.));
#17950=DIRECTION('ref_axis',(0.,0.906392585430544,-0.422436363345457));
#17951=DIRECTION('',(-1.,0.,0.));
#17952=DIRECTION('center_axis',(1.,0.,0.));
#17953=DIRECTION('ref_axis',(0.,0.393919298579167,0.919145030018058));
#17954=DIRECTION('center_axis',(1.,0.,0.));
#17955=DIRECTION('ref_axis',(0.,0.393919298579167,0.919145030018058));
#17956=DIRECTION('',(1.,0.,0.));
#17957=DIRECTION('center_axis',(1.,0.,0.));
#17958=DIRECTION('ref_axis',(0.,0.393919298579167,0.919145030018058));
#17959=DIRECTION('center_axis',(1.,0.,0.));
#17960=DIRECTION('ref_axis',(0.,-0.919145030018058,0.393919298579167));
#17961=DIRECTION('center_axis',(1.,0.,0.));
#17962=DIRECTION('ref_axis',(0.,0.919145030018058,-0.393919298579167));
#17963=DIRECTION('',(-1.,0.,0.));
#17964=DIRECTION('center_axis',(1.,0.,0.));
#17965=DIRECTION('ref_axis',(0.,0.919145030018058,-0.393919298579167));
#17966=DIRECTION('',(-1.,0.,0.));
#17967=DIRECTION('center_axis',(1.,0.,0.));
#17968=DIRECTION('ref_axis',(0.,0.919145030018058,-0.393919298579167));
#17969=DIRECTION('center_axis',(1.,0.,0.));
#17970=DIRECTION('ref_axis',(0.,-0.919145030018058,0.393919298579167));
#17971=DIRECTION('',(-1.,0.,0.));
#17972=DIRECTION('center_axis',(1.,0.,0.));
#17973=DIRECTION('ref_axis',(0.,-0.919145030018058,0.393919298579167));
#17974=DIRECTION('',(-1.,0.,0.));
#17975=DIRECTION('center_axis',(1.,0.,0.));
#17976=DIRECTION('ref_axis',(0.,0.393919298579167,0.919145030018058));
#17977=DIRECTION('center_axis',(-1.,0.,0.));
#17978=DIRECTION('ref_axis',(0.,-0.919145030018058,0.393919298579167));
#17979=DIRECTION('',(-1.,0.,0.));
#17980=DIRECTION('center_axis',(-1.,0.,0.));
#17981=DIRECTION('ref_axis',(0.,-0.919145030018058,0.393919298579167));
#17982=DIRECTION('center_axis',(-1.,0.,0.));
#17983=DIRECTION('ref_axis',(0.,-0.919145030018058,0.393919298579167));
#17984=DIRECTION('',(-1.,0.,0.));
#17985=DIRECTION('center_axis',(-1.04183445162406E-32,0.745459602640149,
0.666550808889758));
#17986=DIRECTION('ref_axis',(1.,2.2658674387795E-32,-9.71086045191213E-33));
#17987=DIRECTION('',(-1.,-2.2658674387795E-32,9.71086045191211E-33));
#17988=DIRECTION('',(3.69778549322349E-32,-0.666550808889758,0.745459602640149));
#17989=DIRECTION('',(-1.,-2.2658674387795E-32,9.71086045191211E-33));
#17990=DIRECTION('',(3.69778549322349E-32,-0.666550808889758,0.745459602640149));
#17991=DIRECTION('center_axis',(-1.,-2.46476191160893E-32,2.75654970442689E-32));
#17992=DIRECTION('ref_axis',(-3.35133178729961E-32,0.919145030018058,-0.393919298579167));
#17993=DIRECTION('',(0.,-0.745459602640149,-0.666550808889759));
#17994=DIRECTION('',(0.,-0.745459602640149,-0.666550808889759));
#17995=DIRECTION('',(3.69778549322349E-32,-0.666550808889758,0.745459602640149));
#17996=DIRECTION('center_axis',(1.04183445162406E-32,-0.745459602640149,
-0.666550808889758));
#17997=DIRECTION('ref_axis',(4.49774480223914E-49,-0.666550808889758,0.745459602640149));
#17998=DIRECTION('',(1.,2.2658674387795E-32,-9.71086045191211E-33));
#17999=DIRECTION('',(1.,2.2658674387795E-32,-9.71086045191211E-33));
#18000=DIRECTION('',(3.69778549322349E-32,-0.666550808889758,0.745459602640149));
#18001=DIRECTION('center_axis',(0.,-0.666550808889759,0.745459602640149));
#18002=DIRECTION('ref_axis',(-1.,0.,0.));
#18003=DIRECTION('',(-4.93038065763132E-32,0.745459602640149,0.666550808889759));
#18004=DIRECTION('',(1.,2.2658674387795E-32,-9.71086045191211E-33));
#18005=DIRECTION('',(0.,-0.745459602640149,-0.666550808889759));
#18006=DIRECTION('',(-1.,1.17200666323663E-15,1.0479467789238E-15));
#18007=DIRECTION('center_axis',(1.04183445162406E-32,-0.745459602640149,
-0.666550808889758));
#18008=DIRECTION('ref_axis',(4.49774480223914E-49,-0.666550808889758,0.745459602640149));
#18009=DIRECTION('',(1.,2.2658674387795E-32,-9.71086045191211E-33));
#18010=DIRECTION('',(3.69778549322349E-32,-0.666550808889758,0.745459602640149));
#18011=DIRECTION('',(3.69778549322349E-32,-0.666550808889758,0.745459602640149));
#18012=DIRECTION('center_axis',(1.57219339463306E-15,0.745459602640149,
0.666550808889758));
#18013=DIRECTION('ref_axis',(1.,-3.41933578296442E-15,1.46542962127046E-15));
#18014=DIRECTION('',(-1.,1.17200666323663E-15,1.0479467789238E-15));
#18015=DIRECTION('',(3.69778549322349E-32,-0.666550808889758,0.745459602640149));
#18016=DIRECTION('',(3.69778549322349E-32,-0.666550808889758,0.745459602640149));
#18017=DIRECTION('center_axis',(0.,0.745459602640149,0.666550808889759));
#18018=DIRECTION('ref_axis',(1.,0.,0.));
#18019=DIRECTION('',(-1.,0.,0.));
#18020=DIRECTION('',(0.,0.666550808889759,-0.745459602640149));
#18021=DIRECTION('',(0.529728772330716,0.565346465888128,-0.632274308566145));
#18022=DIRECTION('',(0.,-0.666550808889759,0.745459602640149));
#18023=DIRECTION('center_axis',(1.,0.,0.));
#18024=DIRECTION('ref_axis',(0.,-0.393919298579167,-0.919145030018058));
#18025=DIRECTION('',(0.,0.745459602640149,0.666550808889759));
#18026=DIRECTION('',(0.,-0.666550808889759,0.745459602640149));
#18027=DIRECTION('',(0.,0.745459602640149,0.666550808889759));
#18028=DIRECTION('',(0.,0.666550808889759,-0.745459602640149));
#18029=DIRECTION('center_axis',(0.848167098963991,-0.353091141689218,0.39489140012871));
#18030=DIRECTION('ref_axis',(-0.492600338968907,-0.799891160660238,0.342810497425816));
#18031=DIRECTION('',(-0.468106510930722,-0.15062637763103,0.870739908805161));
#18032=DIRECTION('',(0.468106510930722,0.848535364894395,-0.246706361790292));
#18033=DIRECTION('',(0.529728772330716,0.565346465888128,-0.632274308566145));
#18034=DIRECTION('',(0.,0.745459602640149,0.666550808889759));
#18035=DIRECTION('center_axis',(0.,0.666550808889759,-0.745459602640149));
#18036=DIRECTION('ref_axis',(1.,0.,0.));
#18037=DIRECTION('',(0.707106781186548,-0.527119540127478,-0.471322596971327));
#18038=DIRECTION('',(-1.,0.,0.));
#18039=DIRECTION('',(0.,-0.745459602640149,-0.666550808889759));
#18040=DIRECTION('',(1.,0.,0.));
#18041=DIRECTION('',(-1.,0.,0.));
#18042=DIRECTION('',(-0.707106781186549,-0.527119540127477,-0.471322596971326));
#18043=DIRECTION('center_axis',(0.,-0.745459602640149,-0.666550808889759));
#18044=DIRECTION('ref_axis',(0.,-0.666550808889759,0.745459602640149));
#18045=DIRECTION('',(1.,0.,0.));
#18046=DIRECTION('',(0.,-0.666550808889759,0.745459602640149));
#18047=DIRECTION('',(0.,-0.666550808889759,0.745459602640149));
#18048=DIRECTION('center_axis',(0.,0.745459602640149,0.666550808889759));
#18049=DIRECTION('ref_axis',(1.,0.,0.));
#18050=DIRECTION('',(-1.,0.,0.));
#18051=DIRECTION('',(0.,-0.666550808889759,0.745459602640149));
#18052=DIRECTION('',(0.,-0.666550808889759,0.745459602640149));
#18053=DIRECTION('center_axis',(-6.83191888629751E-32,-0.666550808889759,
0.745459602640149));
#18054=DIRECTION('ref_axis',(-1.,6.92868844298358E-32,-2.96943790413582E-32));
#18055=DIRECTION('center_axis',(6.83191888629751E-32,0.666550808889759,
-0.745459602640149));
#18056=DIRECTION('ref_axis',(-3.90611085686253E-47,0.745459602640149,0.666550808889759));
#18057=DIRECTION('',(9.16407275022627E-16,-0.745459602640149,-0.666550808889759));
#18058=DIRECTION('',(9.16407275022627E-16,-0.745459602640149,-0.666550808889759));
#18059=DIRECTION('',(9.16407275022627E-16,-0.745459602640149,-0.666550808889759));
#18060=DIRECTION('',(9.16407275022627E-16,-0.745459602640149,-0.666550808889759));
#18061=DIRECTION('center_axis',(6.83191888629751E-32,0.666550808889759,
-0.745459602640149));
#18062=DIRECTION('ref_axis',(-8.13589634095566E-47,0.745459602640149,0.666550808889759));
#18063=DIRECTION('',(9.16407275022627E-16,-0.745459602640149,-0.666550808889759));
#18064=DIRECTION('center_axis',(-0.918412615811006,-0.26370342792269,0.294921632338166));
#18065=DIRECTION('ref_axis',(3.6676144219822E-17,0.745459602640148,0.66655080888976));
#18066=DIRECTION('',(-0.393983915184351,0.541825269129043,-0.742429829889162));
#18067=DIRECTION('',(9.16407275022627E-16,-0.745459602640149,-0.666550808889759));
#18068=DIRECTION('',(-0.395623896041664,0.612168671963385,-0.684639503642172));
#18069=DIRECTION('center_axis',(0.918412615811007,0.263703427922722,-0.294921632338134));
#18070=DIRECTION('ref_axis',(0.395623896041661,-0.61216867196347,0.684639503642098));
#18071=DIRECTION('center_axis',(0.91841261581104,0.26370342792224,-0.294921632338462));
#18072=DIRECTION('ref_axis',(0.395623896041585,-0.612168671941529,0.684639503661761));
#18073=DIRECTION('center_axis',(0.,0.666550808889759,-0.745459602640149));
#18074=DIRECTION('ref_axis',(1.,0.,0.));
#18075=DIRECTION('',(-1.,0.,0.));
#18076=DIRECTION('',(-3.46944695195361E-15,0.745459602640149,0.666550808889759));
#18077=DIRECTION('',(0.974370064785235,0.16769192358466,0.149941307233507));
#18078=DIRECTION('',(0.,-0.745459602640149,-0.666550808889759));
#18079=DIRECTION('',(-1.,0.,0.));
#18080=DIRECTION('',(0.,-0.745459602640149,-0.666550808889759));
#18081=DIRECTION('center_axis',(1.,-2.15204789668062E-15,-1.92424815673669E-15));
#18082=DIRECTION('ref_axis',(-2.61639632775514E-15,-0.393919298579167,-0.919145030018058));
#18083=DIRECTION('',(5.91645678915759E-31,-0.666550808889758,0.745459602640149));
#18084=DIRECTION('',(-1.22004564440084E-15,0.289055347086673,-0.957312387008861));
#18085=DIRECTION('',(2.88687393529957E-15,0.745459602640149,0.666550808889758));
#18086=DIRECTION('',(-1.22004564440084E-15,-0.919145030018058,0.393919298579168));
#18087=DIRECTION('',(5.91645678915759E-31,-0.666550808889758,0.745459602640149));
#18088=DIRECTION('',(2.88687393529957E-15,0.745459602640149,0.666550808889758));
#18089=DIRECTION('center_axis',(6.4557060863977E-15,0.745459602640149,0.666550808889758));
#18090=DIRECTION('ref_axis',(1.,-1.40404017094047E-14,6.0173150183163E-15));
#18091=DIRECTION('',(1.,-4.81246809392762E-15,-4.30305611384292E-15));
#18092=DIRECTION('',(5.91645678915759E-31,-0.666550808889758,0.745459602640149));
#18093=DIRECTION('',(-1.,4.81246809392762E-15,4.30305611384292E-15));
#18094=DIRECTION('center_axis',(6.73294499808335E-16,0.745459602640149,
0.666550808889758));
#18095=DIRECTION('ref_axis',(1.,-1.46433637460046E-15,6.27572731971625E-16));
#18096=DIRECTION('',(5.91645678915759E-31,-0.666550808889758,0.745459602640149));
#18097=DIRECTION('',(1.,-5.0191385028692E-16,-4.48784993468273E-16));
#18098=DIRECTION('',(5.91645678915759E-31,-0.666550808889758,0.745459602640149));
#18099=DIRECTION('',(-1.,5.01913850286919E-16,4.48784993468272E-16));
#18100=DIRECTION('center_axis',(-1.,3.2296864575908E-15,2.88781593683036E-15));
#18101=DIRECTION('ref_axis',(-3.92655748994937E-15,-0.393919298579167,-0.919145030018058));
#18102=DIRECTION('',(-4.33247683194691E-15,-0.745459602640149,-0.666550808889758));
#18103=DIRECTION('',(1.83098382774925E-15,-0.289055347086674,0.95731238700886));
#18104=DIRECTION('',(5.91645678915759E-31,-0.666550808889758,0.745459602640149));
#18105=DIRECTION('',(-4.33247683194691E-15,-0.745459602640149,-0.666550808889758));
#18106=DIRECTION('',(1.83098382774927E-15,0.919145030018059,-0.393919298579165));
#18107=DIRECTION('center_axis',(-5.85085669692213E-15,-0.393919298579168,
-0.919145030018058));
#18108=DIRECTION('ref_axis',(2.88250692241653E-32,-0.919145030018058,0.393919298579168));
#18109=DIRECTION('',(1.22004564440084E-15,0.919145030018058,-0.393919298579168));
#18110=DIRECTION('',(-1.,4.81246809392762E-15,4.30305611384292E-15));
#18111=DIRECTION('center_axis',(6.10212048145241E-16,0.957312387008861,
0.289055347086673));
#18112=DIRECTION('ref_axis',(1.,-3.73956028970675E-16,-8.72564067598243E-16));
#18113=DIRECTION('',(-1.,5.0191385028692E-16,4.48784993468273E-16));
#18114=DIRECTION('',(1.22004564440084E-15,-0.289055347086673,0.957312387008861));
#18115=DIRECTION('',(1.,-5.0191385028692E-16,-4.48784993468273E-16));
#18116=DIRECTION('center_axis',(-9.86076131526264E-31,0.666550808889758,
-0.745459602640149));
#18117=DIRECTION('ref_axis',(1.,-9.19114135003496E-31,-2.14459964834149E-30));
#18118=DIRECTION('',(-2.88687393529957E-15,-0.745459602640149,-0.666550808889758));
#18119=DIRECTION('center_axis',(-6.10212048145241E-16,-0.393919298579165,
-0.919145030018059));
#18120=DIRECTION('ref_axis',(1.,-2.4037430198993E-16,-5.60873371309838E-16));
#18121=DIRECTION('',(-1.22004564440084E-15,-0.919145030018059,0.393919298579165));
#18122=DIRECTION('',(-1.,5.0191385028692E-16,4.48784993468273E-16));
#18123=DIRECTION('center_axis',(6.10212048145256E-16,0.957312387008861,
0.289055347086674));
#18124=DIRECTION('ref_axis',(1.,-3.73956028970684E-16,-8.72564067598264E-16));
#18125=DIRECTION('',(-1.22004564440084E-15,0.289055347086674,-0.95731238700886));
#18126=DIRECTION('',(-1.,5.01913850286932E-16,4.48784993468284E-16));
#18127=DIRECTION('',(1.,-5.01913850286932E-16,-4.48784993468284E-16));
#18128=DIRECTION('center_axis',(-2.23422119153307E-32,0.666550808889759,
-0.745459602640149));
#18129=DIRECTION('ref_axis',(1.,-2.08250074432281E-32,-4.8591684034199E-32));
#18130=DIRECTION('',(0.,0.745459602640149,0.666550808889759));
#18131=DIRECTION('center_axis',(0.,0.666550808889759,-0.745459602640149));
#18132=DIRECTION('ref_axis',(0.,-0.745459602640149,-0.666550808889759));
#18133=DIRECTION('',(0.173648177666931,-0.656424404371193,0.734134396237418));
#18134=DIRECTION('center_axis',(0.,-0.666550808889759,0.745459602640149));
#18135=DIRECTION('ref_axis',(0.,0.745459602640149,0.666550808889759));
#18136=DIRECTION('',(0.,0.785872105893968,-0.618389062951294));
#18137=DIRECTION('center_axis',(0.,0.666550808889759,-0.745459602640149));
#18138=DIRECTION('ref_axis',(0.,0.745459602640149,0.666550808889759));
#18139=DIRECTION('center_axis',(2.46383476629014E-15,0.618389062951294,
0.785872105893968));
#18140=DIRECTION('ref_axis',(1.,-8.74982549805887E-15,3.74992521345379E-15));
#18141=DIRECTION('',(-1.,1.86502317861713E-15,1.66760573464032E-15));
#18142=DIRECTION('',(1.00410523453136E-15,0.785872105893969,-0.618389062951293));
#18143=DIRECTION('',(1.,-1.86502317861713E-15,-1.66760573464032E-15));
#18144=DIRECTION('center_axis',(-0.984807753012208,-0.115745333286125,0.129447701522776));
#18145=DIRECTION('ref_axis',(1.45875349239297E-18,0.74545960264015,0.666550808889758));
#18146=DIRECTION('',(1.80700362080917E-16,0.745459602640149,0.666550808889759));
#18147=DIRECTION('',(0.173648177666931,-0.656424404371193,0.734134396237418));
#18148=DIRECTION('',(-1.80700362080917E-16,-0.745459602640149,-0.666550808889759));
#18149=DIRECTION('center_axis',(0.,0.666550808889759,-0.745459602640149));
#18150=DIRECTION('ref_axis',(0.,-0.745459602640149,-0.666550808889759));
#18151=DIRECTION('center_axis',(0.,-0.666550808889759,0.745459602640149));
#18152=DIRECTION('ref_axis',(0.,0.745459602640149,0.666550808889759));
#18153=DIRECTION('',(0.173648177666932,0.656424404371191,-0.73413439623742));
#18154=DIRECTION('center_axis',(0.,0.666550808889759,-0.745459602640149));
#18155=DIRECTION('ref_axis',(0.,0.745459602640149,0.666550808889759));
#18156=DIRECTION('center_axis',(0.,0.666550808889758,-0.745459602640149));
#18157=DIRECTION('ref_axis',(0.,-0.745459602640149,-0.666550808889758));
#18158=DIRECTION('center_axis',(0.,0.666550808889758,-0.745459602640149));
#18159=DIRECTION('ref_axis',(0.,0.745459602640149,0.666550808889758));
#18160=DIRECTION('',(0.,-0.526976702848416,0.849879729523544));
#18161=DIRECTION('center_axis',(0.,-0.666550808889759,0.745459602640149));
#18162=DIRECTION('ref_axis',(0.,0.745459602640149,0.666550808889759));
#18163=DIRECTION('center_axis',(0.984807753012208,-0.115745333286128,0.129447701522774));
#18164=DIRECTION('ref_axis',(-0.157804207302256,-0.907628529662534,0.388983655569657));
#18165=DIRECTION('',(3.61400724161834E-15,0.745459602640149,0.666550808889759));
#18166=DIRECTION('',(0.173648177666931,0.656424404371193,-0.734134396237418));
#18167=DIRECTION('',(-3.61400724161834E-15,-0.745459602640149,-0.666550808889759));
#18168=DIRECTION('center_axis',(-2.6834563621475E-15,-0.849879729523544,
-0.526976702848416));
#18169=DIRECTION('ref_axis',(-1.63031537087573E-31,-0.526976702848416,0.849879729523544));
#18170=DIRECTION('',(-1.,2.03126783609293E-15,1.81625297256125E-15));
#18171=DIRECTION('',(0.,-0.526976702848416,0.849879729523544));
#18172=DIRECTION('',(1.,-2.03126783609293E-15,-1.81625297256125E-15));
#18173=DIRECTION('center_axis',(-6.73294499808353E-16,-0.745459602640149,
-0.666550808889758));
#18174=DIRECTION('ref_axis',(2.12962857256229E-32,-0.666550808889758,0.745459602640149));
#18175=DIRECTION('',(5.91645678915759E-31,-0.666550808889758,0.745459602640149));
#18176=DIRECTION('',(1.,-5.01913850286932E-16,-4.48784993468284E-16));
#18177=DIRECTION('center_axis',(0.,0.66655080888976,-0.745459602640148));
#18178=DIRECTION('ref_axis',(0.,-0.745459602640148,-0.66655080888976));
#18179=DIRECTION('center_axis',(0.,-0.666550808889759,0.745459602640149));
#18180=DIRECTION('ref_axis',(0.,0.745459602640149,0.666550808889759));
#18181=DIRECTION('center_axis',(0.,0.66655080888976,-0.745459602640148));
#18182=DIRECTION('ref_axis',(0.,0.745459602640148,0.66655080888976));
#18183=DIRECTION('center_axis',(1.,6.14016151751146E-32,5.29799511051683E-33));
#18184=DIRECTION('ref_axis',(2.90569070563006E-32,-0.393919298579167,-0.919145030018058));
#18185=DIRECTION('',(-4.93038065763132E-32,0.745459602640149,0.666550808889759));
#18186=DIRECTION('center_axis',(0.,0.745459602640149,0.666550808889759));
#18187=DIRECTION('ref_axis',(1.,0.,0.));
#18188=DIRECTION('',(0.,-0.666550808889759,0.745459602640149));
#18189=DIRECTION('',(0.,-0.666550808889759,0.745459602640149));
#18190=DIRECTION('center_axis',(-0.707106781186546,0.527119540127479,0.471322596971328));
#18191=DIRECTION('ref_axis',(-6.76209254941581E-18,0.666550808889759,-0.745459602640149));
#18192=DIRECTION('center_axis',(0.707106781186548,0.527119540127479,0.471322596971327));
#18193=DIRECTION('ref_axis',(0.389281620635025,-0.846641755162944,0.362846466498404));
#18194=DIRECTION('center_axis',(0.,0.365017828521802,0.931000528926396));
#18195=DIRECTION('ref_axis',(-1.,0.,0.));
#18196=DIRECTION('',(0.,0.931000528926396,-0.365017828521802));
#18197=DIRECTION('',(-1.,0.,0.));
#18198=DIRECTION('',(0.,0.931000528926396,-0.365017828521802));
#18199=DIRECTION('',(0.,0.931000528926396,-0.365017828521802));
#18200=DIRECTION('',(0.,0.931000528926396,-0.365017828521802));
#18201=DIRECTION('center_axis',(0.,0.919145030018058,-0.393919298579167));
#18202=DIRECTION('ref_axis',(-1.,0.,0.));
#18203=DIRECTION('',(0.,-0.393919298579167,-0.919145030018058));
#18204=DIRECTION('',(0.,-0.393919298579167,-0.919145030018058));
#18205=DIRECTION('',(-1.,0.,0.));
#18206=DIRECTION('center_axis',(1.,0.,0.));
#18207=DIRECTION('ref_axis',(0.,0.3568432321356,-0.934164283024682));
#18208=DIRECTION('center_axis',(-1.,0.,0.));
#18209=DIRECTION('ref_axis',(0.,0.919145030018058,-0.393919298579167));
#18210=DIRECTION('center_axis',(-1.,0.,0.));
#18211=DIRECTION('ref_axis',(0.,0.919145030018058,-0.393919298579167));
#18212=DIRECTION('',(-1.,0.,0.));
#18213=DIRECTION('center_axis',(0.,-0.422436363345456,-0.906392585430544));
#18214=DIRECTION('ref_axis',(0.,-0.906392585430544,0.422436363345456));
#18215=DIRECTION('',(0.,-0.906392585430544,0.422436363345457));
#18216=DIRECTION('',(0.,-0.906392585430544,0.422436363345457));
#18217=DIRECTION('',(0.,-0.906392585430544,0.422436363345456));
#18218=DIRECTION('',(-1.,0.,0.));
#18219=DIRECTION('center_axis',(1.,0.,0.));
#18220=DIRECTION('ref_axis',(0.,0.393919298579167,0.919145030018058));
#18221=DIRECTION('center_axis',(-1.,0.,0.));
#18222=DIRECTION('ref_axis',(0.,0.919145030018058,-0.393919298579167));
#18223=DIRECTION('center_axis',(-1.,0.,0.));
#18224=DIRECTION('ref_axis',(0.,0.919145030018058,-0.393919298579167));
#18225=DIRECTION('',(-1.,0.,0.));
#18226=DIRECTION('center_axis',(1.,0.,0.));
#18227=DIRECTION('ref_axis',(0.,0.393919298579167,0.919145030018058));
#18228=DIRECTION('center_axis',(-1.,0.,0.));
#18229=DIRECTION('ref_axis',(0.,0.919145030018058,-0.393919298579167));
#18230=DIRECTION('',(-1.,0.,0.));
#18231=DIRECTION('center_axis',(-1.,0.,0.));
#18232=DIRECTION('ref_axis',(0.,0.919145030018058,-0.393919298579167));
#18233=DIRECTION('center_axis',(0.,-0.919145030018058,0.393919298579167));
#18234=DIRECTION('ref_axis',(0.,0.393919298579167,0.919145030018058));
#18235=DIRECTION('',(0.,0.393919298579167,0.919145030018058));
#18236=DIRECTION('',(0.,0.393919298579167,0.919145030018058));
#18237=DIRECTION('center_axis',(1.,0.,0.));
#18238=DIRECTION('ref_axis',(0.,0.393919298579168,0.919145030018058));
#18239=DIRECTION('center_axis',(-1.,0.,0.));
#18240=DIRECTION('ref_axis',(0.,0.919145030018059,-0.393919298579166));
#18241=DIRECTION('',(-1.,0.,0.));
#18242=DIRECTION('center_axis',(-1.,0.,0.));
#18243=DIRECTION('ref_axis',(0.,0.919145030018059,-0.393919298579166));
#18244=DIRECTION('center_axis',(1.,0.,0.));
#18245=DIRECTION('ref_axis',(0.,0.393919298579168,0.919145030018058));
#18246=DIRECTION('center_axis',(-1.,0.,0.));
#18247=DIRECTION('ref_axis',(0.,0.919145030018058,-0.393919298579167));
#18248=DIRECTION('center_axis',(-1.,0.,0.));
#18249=DIRECTION('ref_axis',(0.,0.919145030018058,-0.393919298579167));
#18250=DIRECTION('',(-1.,0.,0.));
#18251=DIRECTION('center_axis',(0.,-0.39391929857917,-0.919145030018057));
#18252=DIRECTION('ref_axis',(0.,-0.919145030018057,0.39391929857917));
#18253=DIRECTION('',(0.,-0.919145030018057,0.39391929857917));
#18254=DIRECTION('',(0.,-0.919145030018057,0.39391929857917));
#18255=DIRECTION('',(-1.,0.,0.));
#18256=DIRECTION('center_axis',(1.,0.,0.));
#18257=DIRECTION('ref_axis',(0.,0.393919298579168,0.919145030018058));
#18258=DIRECTION('center_axis',(-1.,0.,0.));
#18259=DIRECTION('ref_axis',(0.,0.919145030018058,-0.393919298579167));
#18260=DIRECTION('center_axis',(-1.,0.,0.));
#18261=DIRECTION('ref_axis',(0.,0.919145030018058,-0.393919298579167));
#18262=DIRECTION('center_axis',(1.,0.,0.));
#18263=DIRECTION('ref_axis',(0.,0.393919298579168,0.919145030018058));
#18264=DIRECTION('center_axis',(-1.,0.,0.));
#18265=DIRECTION('ref_axis',(0.,0.919145030018059,-0.393919298579166));
#18266=DIRECTION('center_axis',(-1.,0.,0.));
#18267=DIRECTION('ref_axis',(0.,0.919145030018059,-0.393919298579166));
#18268=DIRECTION('',(-1.,0.,0.));
#18269=DIRECTION('center_axis',(-1.,0.,0.));
#18270=DIRECTION('ref_axis',(0.,0.919145030018058,-0.393919298579167));
#18271=DIRECTION('',(0.,0.666550808889759,-0.745459602640149));
#18272=DIRECTION('center_axis',(-1.,0.,0.));
#18273=DIRECTION('ref_axis',(0.,0.919145030018058,-0.393919298579167));
#18274=DIRECTION('',(0.,0.919145030018057,-0.39391929857917));
#18275=DIRECTION('center_axis',(-1.,0.,0.));
#18276=DIRECTION('ref_axis',(0.,0.919145030018058,-0.393919298579167));
#18277=DIRECTION('',(0.,0.919145030018057,-0.39391929857917));
#18278=DIRECTION('center_axis',(0.,0.39391929857917,0.919145030018057));
#18279=DIRECTION('ref_axis',(0.,0.919145030018057,-0.39391929857917));
#18280=DIRECTION('center_axis',(0.,0.666550808889759,-0.745459602640149));
#18281=DIRECTION('ref_axis',(1.,0.,0.));
#18282=DIRECTION('',(0.,-0.745459602640149,-0.666550808889759));
#18283=DIRECTION('center_axis',(0.,-0.666550808889758,0.745459602640149));
#18284=DIRECTION('ref_axis',(0.,0.745459602640149,0.666550808889758));
#18285=DIRECTION('',(1.,0.,0.));
#18286=DIRECTION('',(0.,-0.745459602640149,-0.666550808889759));
#18287=DIRECTION('',(-1.,0.,0.));
#18288=DIRECTION('center_axis',(-1.,0.,0.));
#18289=DIRECTION('ref_axis',(0.,0.919145030018058,-0.393919298579167));
#18290=DIRECTION('',(0.,-0.666550808889758,0.745459602640149));
#18291=DIRECTION('center_axis',(0.,0.745459602640149,0.666550808889759));
#18292=DIRECTION('ref_axis',(1.,0.,0.));
#18293=DIRECTION('',(0.,0.666550808889759,-0.745459602640149));
#18294=DIRECTION('',(0.707106781186549,0.471322596971326,-0.527119540127477));
#18295=DIRECTION('',(1.,6.2631905706088E-16,-7.00465064591613E-16));
#18296=DIRECTION('',(0.,0.666550808889759,-0.745459602640149));
#18297=DIRECTION('',(0.,0.666550808889759,-0.745459602640149));
#18298=DIRECTION('',(-1.,0.,0.));
#18299=DIRECTION('center_axis',(-1.,0.,0.));
#18300=DIRECTION('ref_axis',(0.,0.919145030018058,-0.393919298579167));
#18301=DIRECTION('center_axis',(0.,0.666550808889759,-0.745459602640149));
#18302=DIRECTION('ref_axis',(1.,0.,0.));
#18303=DIRECTION('',(-0.974370064785235,0.16769192358466,0.149941307233508));
#18304=DIRECTION('',(3.46944695195361E-15,0.745459602640149,0.666550808889759));
#18305=DIRECTION('',(-1.,3.30366096032112E-16,-3.69476078026345E-16));
#18306=DIRECTION('',(0.,0.745459602640149,0.666550808889759));
#18307=DIRECTION('',(0.,-0.745459602640149,-0.666550808889759));
#18308=DIRECTION('center_axis',(0.,-0.745459602640149,-0.666550808889758));
#18309=DIRECTION('ref_axis',(0.,-0.666550808889758,0.745459602640149));
#18310=DIRECTION('',(0.707106781186547,0.471322596971327,-0.527119540127479));
#18311=DIRECTION('',(0.,0.666550808889758,-0.745459602640149));
#18312=DIRECTION('',(0.,-0.666550808889758,0.745459602640149));
#18313=DIRECTION('',(0.,-0.666550808889758,0.745459602640149));
#18314=DIRECTION('',(1.,1.92713556018732E-16,-2.15527712182035E-16));
#18315=DIRECTION('center_axis',(-1.,0.,0.));
#18316=DIRECTION('ref_axis',(0.,0.919145030018058,-0.393919298579167));
#18317=DIRECTION('',(0.,0.745459602640149,0.666550808889759));
#18318=DIRECTION('',(0.,-0.666550808889759,0.745459602640149));
#18319=DIRECTION('',(0.,-0.745459602640149,-0.666550808889759));
#18320=DIRECTION('',(0.,-0.666550808889759,0.745459602640149));
#18321=DIRECTION('',(0.,-0.745459602640149,-0.666550808889759));
#18322=DIRECTION('',(0.,-0.666550808889759,0.745459602640149));
#18323=DIRECTION('',(0.,-0.666550808889758,0.745459602640149));
#18324=DIRECTION('',(0.,-0.745459602640149,-0.666550808889759));
#18325=DIRECTION('center_axis',(-1.,0.,0.));
#18326=DIRECTION('ref_axis',(0.,0.919145030018058,-0.393919298579167));
#18327=DIRECTION('',(0.,-0.745459602640149,-0.666550808889759));
#18328=DIRECTION('',(0.,-0.745459602640149,-0.666550808889759));
#18329=DIRECTION('',(0.,-0.745459602640149,-0.666550808889759));
#18330=DIRECTION('center_axis',(-0.707106781186548,0.471322596971326,-0.527119540127479));
#18331=DIRECTION('ref_axis',(5.73427809096105E-17,-0.745459602640149,-0.666550808889758));
#18332=DIRECTION('',(0.,-0.745459602640149,-0.666550808889759));
#18333=DIRECTION('',(0.707106781186547,0.471322596971327,-0.527119540127479));
#18334=DIRECTION('',(0.,-0.745459602640149,-0.666550808889759));
#18335=DIRECTION('center_axis',(-1.,0.,0.));
#18336=DIRECTION('ref_axis',(0.,0.919145030018058,-0.393919298579167));
#18337=DIRECTION('',(0.,0.666550808889758,-0.745459602640149));
#18338=DIRECTION('center_axis',(-2.89120579329468E-16,0.666550808889759,
-0.745459602640149));
#18339=DIRECTION('ref_axis',(1.,-2.69487114317234E-16,-6.28803266740213E-16));
#18340=DIRECTION('',(1.,1.92713556018732E-16,-2.15527712182035E-16));
#18341=DIRECTION('center_axis',(7.85046229341889E-17,0.745459602640149,
0.666550808889758));
#18342=DIRECTION('ref_axis',(1.,-1.70738324714595E-16,7.31735677348263E-17));
#18343=DIRECTION('',(-1.,0.,0.));
#18344=DIRECTION('center_axis',(0.707106781186547,-0.471322596971327,0.527119540127479));
#18345=DIRECTION('ref_axis',(-0.671542934237819,-0.681054890267067,0.291880667257314));
#18346=DIRECTION('',(0.,0.745459602640149,0.666550808889759));
#18347=DIRECTION('',(0.707106781186549,0.471322596971326,-0.527119540127477));
#18348=DIRECTION('',(0.,0.745459602640149,0.666550808889759));
#18349=DIRECTION('center_axis',(1.,0.,0.));
#18350=DIRECTION('ref_axis',(0.,-0.393919298579167,-0.919145030018058));
#18351=DIRECTION('',(0.,0.666550808889759,-0.745459602640149));
#18352=DIRECTION('center_axis',(9.39641882820771E-16,-0.666550808889759,
0.745459602640149));
#18353=DIRECTION('ref_axis',(-1.,-9.52951280949986E-16,4.08407691835707E-16));
#18354=DIRECTION('',(1.,6.2631905706088E-16,-7.00465064591613E-16));
#18355=DIRECTION('center_axis',(0.,0.745459602640149,0.666550808889759));
#18356=DIRECTION('ref_axis',(1.,0.,0.));
#18357=DIRECTION('',(-1.,3.30366096032112E-16,-3.69476078026345E-16));
#18358=DIRECTION('',(-1.,3.30366096032112E-16,-3.69476078026345E-16));
#18359=DIRECTION('center_axis',(1.,-2.58633254618441E-15,-2.31256267222479E-15));
#18360=DIRECTION('ref_axis',(-3.14438678926613E-15,-0.393919298579167,-0.919145030018058));
#18361=DIRECTION('',(0.,-0.666550808889759,0.745459602640149));
#18362=DIRECTION('',(3.46944695195361E-15,0.745459602640149,0.666550808889759));
#18363=DIRECTION('',(0.,-0.666550808889759,0.745459602640149));
#18364=DIRECTION('',(3.46944695195361E-15,0.745459602640149,0.666550808889759));
#18365=DIRECTION('center_axis',(-2.45655217911417E-16,0.745459602640149,
0.666550808889759));
#18366=DIRECTION('ref_axis',(1.,5.34271216088195E-16,-2.28973378323512E-16));
#18367=DIRECTION('',(-1.,-1.83126041130723E-16,-1.63741684206845E-16));
#18368=DIRECTION('',(-1.,-1.83126041130723E-16,-1.63741684206845E-16));
#18369=DIRECTION('',(0.,-0.666550808889759,0.745459602640149));
#18370=DIRECTION('center_axis',(-1.,0.,0.));
#18371=DIRECTION('ref_axis',(0.,0.919145030018058,-0.393919298579167));
#18372=DIRECTION('',(0.,-0.745459602640149,-0.666550808889759));
#18373=DIRECTION('',(0.,-0.745459602640149,-0.666550808889759));
#18374=DIRECTION('',(0.,-0.666550808889759,0.745459602640149));
#18375=DIRECTION('',(0.,-0.745459602640149,-0.666550808889759));
#18376=DIRECTION('center_axis',(1.14639101691994E-15,0.745459602640149,
0.666550808889759));
#18377=DIRECTION('ref_axis',(1.,-2.49326567507823E-15,1.06854243217638E-15));
#18378=DIRECTION('',(-1.,8.54588191943377E-16,7.64127859631943E-16));
#18379=DIRECTION('',(-1.,8.54588191943377E-16,7.64127859631943E-16));
#18380=DIRECTION('',(0.,-0.666550808889759,0.745459602640149));
#18381=DIRECTION('center_axis',(0.,0.666550808889758,-0.745459602640149));
#18382=DIRECTION('ref_axis',(0.,0.745459602640149,0.666550808889758));
#18383=DIRECTION('center_axis',(0.,-0.666550808889758,0.745459602640149));
#18384=DIRECTION('ref_axis',(0.,-0.745459602640149,-0.666550808889758));
#18385=DIRECTION('center_axis',(0.,-0.666550808889758,0.745459602640149));
#18386=DIRECTION('ref_axis',(0.,-0.745459602640149,-0.666550808889758));
#18387=DIRECTION('center_axis',(0.,0.666550808889758,-0.745459602640149));
#18388=DIRECTION('ref_axis',(0.,0.745459602640149,0.666550808889758));
#18389=DIRECTION('center_axis',(0.,-0.666550808889758,0.745459602640149));
#18390=DIRECTION('ref_axis',(0.,0.745459602640149,0.666550808889758));
#18391=DIRECTION('',(0.,-0.666550808889759,0.745459602640149));
#18392=DIRECTION('center_axis',(0.,-0.745459602640149,-0.666550808889759));
#18393=DIRECTION('ref_axis',(0.,-0.666550808889759,0.745459602640149));
#18394=DIRECTION('',(1.,0.,0.));
#18395=DIRECTION('',(0.,-0.666550808889759,0.745459602640149));
#18396=DIRECTION('center_axis',(-1.,0.,0.));
#18397=DIRECTION('ref_axis',(0.,0.919145030018058,-0.393919298579167));
#18398=DIRECTION('',(0.,-0.745459602640149,-0.666550808889759));
#18399=DIRECTION('',(0.,-0.666550808889759,0.745459602640149));
#18400=DIRECTION('',(0.,-0.745459602640149,-0.666550808889759));
#18401=DIRECTION('center_axis',(9.16407275022628E-16,-0.745459602640149,
-0.666550808889759));
#18402=DIRECTION('ref_axis',(-5.31053524627771E-32,-0.666550808889759,0.745459602640149));
#18403=DIRECTION('',(1.,6.8314460309491E-16,6.10832010438791E-16));
#18404=DIRECTION('',(1.,6.8314460309491E-16,6.10832010438791E-16));
#18405=DIRECTION('',(0.,-0.666550808889759,0.745459602640149));
#18406=DIRECTION('center_axis',(1.,2.58633254618443E-15,2.31256267222479E-15));
#18407=DIRECTION('ref_axis',(1.46625164003621E-15,-0.919145030018058,0.393919298579167));
#18408=DIRECTION('',(-3.46944695195361E-15,0.745459602640149,0.666550808889759));
#18409=DIRECTION('',(-3.46944695195361E-15,0.745459602640149,0.666550808889759));
#18410=DIRECTION('',(0.,-0.666550808889759,0.745459602640149));
#18411=DIRECTION('center_axis',(0.224951054343865,-0.726353521319258,-0.649467154840565));
#18412=DIRECTION('ref_axis',(1.77259243224035E-17,-0.666550808889758,0.745459602640149));
#18413=DIRECTION('',(0.,-0.666550808889759,0.745459602640149));
#18414=DIRECTION('',(0.974370064785235,0.16769192358466,0.149941307233507));
#18415=DIRECTION('',(0.974370064785235,0.16769192358466,0.149941307233507));
#18416=DIRECTION('center_axis',(0.,-0.666550808889759,0.745459602640149));
#18417=DIRECTION('ref_axis',(-1.,0.,0.));
#18418=DIRECTION('',(1.23259516440783E-32,-0.745459602640149,-0.666550808889759));
#18419=DIRECTION('',(0.,0.745459602640149,0.666550808889759));
#18420=DIRECTION('center_axis',(0.,-0.666550808889759,0.745459602640149));
#18421=DIRECTION('ref_axis',(0.,0.745459602640149,0.666550808889759));
#18422=DIRECTION('',(-0.974370064785235,0.16769192358466,0.149941307233508));
#18423=DIRECTION('',(1.,4.50771793552549E-16,4.0305645343223E-16));
#18424=DIRECTION('center_axis',(0.,0.666550808889758,-0.745459602640149));
#18425=DIRECTION('ref_axis',(0.,0.745459602640149,0.666550808889758));
#18426=DIRECTION('center_axis',(0.,0.666550808889759,-0.745459602640149));
#18427=DIRECTION('ref_axis',(0.,0.745459602640149,0.666550808889759));
#18428=DIRECTION('',(0.,-0.666550808889759,0.745459602640149));
#18429=DIRECTION('center_axis',(0.,-0.666550808889759,0.745459602640149));
#18430=DIRECTION('ref_axis',(0.,0.745459602640149,0.666550808889759));
#18431=DIRECTION('center_axis',(0.,0.666550808889759,-0.745459602640149));
#18432=DIRECTION('ref_axis',(0.,0.745459602640149,0.666550808889759));
#18433=DIRECTION('center_axis',(0.918412615811027,0.263703427922986,-0.294921632337836));
#18434=DIRECTION('ref_axis',(0.395623896041616,-0.612168671944176,0.684639503659376));
#18435=DIRECTION('',(0.,-0.666550808889759,0.745459602640149));
#18436=DIRECTION('',(0.,-0.666550808889759,0.745459602640149));
#18437=DIRECTION('center_axis',(0.,-0.666550808889759,0.745459602640149));
#18438=DIRECTION('ref_axis',(-1.,0.,0.));
#18439=DIRECTION('center_axis',(0.,-0.666550808889759,0.745459602640149));
#18440=DIRECTION('ref_axis',(-1.,0.,0.));
#18441=DIRECTION('',(0.,0.745459602640149,0.666550808889759));
#18442=DIRECTION('',(1.23259516440783E-32,-0.745459602640149,-0.666550808889759));
#18443=DIRECTION('center_axis',(0.,0.666550808889758,-0.745459602640149));
#18444=DIRECTION('ref_axis',(0.,0.745459602640149,0.666550808889758));
#18445=DIRECTION('',(-1.,1.05200988229048E-32,8.90162208091945E-33));
#18446=DIRECTION('center_axis',(0.224951054343865,0.726353521319258,0.649467154840565));
#18447=DIRECTION('ref_axis',(0.877590614935324,-0.44064805168451,0.188849165007647));
#18448=DIRECTION('',(0.393983915184351,-0.677436825736628,0.621173101246256));
#18449=DIRECTION('',(-0.974370064785235,0.16769192358466,0.149941307233508));
#18450=DIRECTION('center_axis',(0.,-0.666550808889759,0.745459602640149));
#18451=DIRECTION('ref_axis',(-1.,0.,0.));
#18452=DIRECTION('',(9.16407275022627E-16,-0.745459602640149,-0.666550808889759));
#18453=DIRECTION('',(1.,4.50771793552549E-16,4.0305645343223E-16));
#18454=DIRECTION('',(3.25260651745651E-15,0.745459602640149,0.666550808889759));
#18455=DIRECTION('',(-1.,1.05200988229048E-32,8.90162208091945E-33));
#18456=DIRECTION('center_axis',(1.,0.,0.));
#18457=DIRECTION('ref_axis',(0.,-0.393919298579167,-0.919145030018058));
#18458=DIRECTION('center_axis',(0.,0.666550808889759,-0.745459602640149));
#18459=DIRECTION('ref_axis',(1.,0.,0.));
#18460=DIRECTION('center_axis',(1.,9.18849901475632E-33,8.21587303869647E-33));
#18461=DIRECTION('ref_axis',(5.20917225812029E-33,-0.919145030018058,0.393919298579167));
#18462=DIRECTION('',(0.,0.666550808889759,-0.745459602640149));
#18463=DIRECTION('center_axis',(0.,-0.666550808889758,0.745459602640149));
#18464=DIRECTION('ref_axis',(0.,-0.745459602640149,-0.666550808889758));
#18465=DIRECTION('',(0.,0.666550808889759,-0.745459602640149));
#18466=DIRECTION('center_axis',(0.918412615811012,0.263703427922711,-0.294921632338128));
#18467=DIRECTION('ref_axis',(0.39562389604165,-0.612168671963492,0.684639503642084));
#18468=DIRECTION('center_axis',(0.,-0.666550808889758,0.745459602640149));
#18469=DIRECTION('ref_axis',(0.,-0.745459602640149,-0.666550808889758));
#18470=DIRECTION('',(0.,0.666550808889759,-0.745459602640149));
#18471=DIRECTION('',(0.,0.666550808889759,-0.745459602640149));
#18472=DIRECTION('center_axis',(-1.37756920867255E-32,-0.745459602640149,
-0.666550808889759));
#18473=DIRECTION('ref_axis',(9.00587119577753E-49,-0.666550808889759,0.745459602640149));
#18474=DIRECTION('',(0.,0.666550808889759,-0.745459602640149));
#18475=DIRECTION('',(-1.,1.05200988229048E-32,8.90162208091945E-33));
#18476=DIRECTION('center_axis',(0.,-0.666550808889759,0.745459602640149));
#18477=DIRECTION('ref_axis',(-1.,0.,0.));
#18478=DIRECTION('center_axis',(-6.04689767166562E-16,0.745459602640149,
0.666550808889759));
#18479=DIRECTION('ref_axis',(1.,1.31512914729401E-15,-5.63626777411718E-16));
#18480=DIRECTION('',(0.395623896041664,-0.612168671963385,0.684639503642172));
#18481=DIRECTION('',(1.,4.50771793552549E-16,4.0305645343223E-16));
#18482=DIRECTION('',(0.,0.666550808889759,-0.745459602640149));
#18483=DIRECTION('center_axis',(-6.16297582203916E-33,0.666550808889759,
-0.745459602640149));
#18484=DIRECTION('ref_axis',(1.,-5.74446334377187E-33,-1.34037478021344E-32));
#18485=DIRECTION('',(3.25260651745651E-15,0.745459602640149,0.666550808889759));
#18486=DIRECTION('center_axis',(-1.,2.42468676204789E-15,2.16802750521074E-15));
#18487=DIRECTION('ref_axis',(-2.947862614937E-15,-0.393919298579167,-0.919145030018058));
#18488=DIRECTION('center_axis',(2.5018433889803E-15,0.745459602640149,0.666550808889759));
#18489=DIRECTION('ref_axis',(1.,-5.44121521723473E-15,2.33194937881488E-15));
#18490=DIRECTION('',(0.,0.666550808889759,-0.745459602640149));
#18491=DIRECTION('',(0.,0.666550808889759,-0.745459602640149));
#18492=DIRECTION('',(1.,-1.86502317861713E-15,-1.66760573464032E-15));
#18493=DIRECTION('center_axis',(0.,-0.666550808889759,0.745459602640149));
#18494=DIRECTION('ref_axis',(0.,-0.745459602640149,-0.666550808889759));
#18495=DIRECTION('',(0.,0.666550808889759,-0.745459602640149));
#18496=DIRECTION('center_axis',(0.,0.666550808889759,-0.745459602640149));
#18497=DIRECTION('ref_axis',(0.,0.745459602640149,0.666550808889759));
#18498=DIRECTION('center_axis',(1.,-2.69409640227544E-15,-2.40891945023415E-15));
#18499=DIRECTION('ref_axis',(-3.27540290548555E-15,-0.393919298579167,-0.919145030018058));
#18500=DIRECTION('',(0.,0.666550808889759,-0.745459602640149));
#18501=DIRECTION('',(-3.61400724161834E-15,-0.745459602640149,-0.666550808889759));
#18502=DIRECTION('center_axis',(0.,-0.666550808889759,0.745459602640149));
#18503=DIRECTION('ref_axis',(0.,-0.745459602640149,-0.666550808889759));
#18504=DIRECTION('',(0.,0.666550808889759,-0.745459602640149));
#18505=DIRECTION('center_axis',(0.,0.666550808889759,-0.745459602640149));
#18506=DIRECTION('ref_axis',(0.,0.745459602640149,0.666550808889759));
#18507=DIRECTION('center_axis',(-2.72485300195868E-15,-0.745459602640149,
-0.666550808889759));
#18508=DIRECTION('ref_axis',(1.46387489158228E-32,-0.666550808889759,0.745459602640149));
#18509=DIRECTION('',(0.,0.666550808889759,-0.745459602640149));
#18510=DIRECTION('',(-1.,2.03126783609293E-15,1.81625297256125E-15));
#18511=DIRECTION('center_axis',(0.,-0.666550808889759,0.745459602640149));
#18512=DIRECTION('ref_axis',(0.,-0.745459602640149,-0.666550808889759));
#18513=DIRECTION('',(0.,0.666550808889759,-0.745459602640149));
#18514=DIRECTION('center_axis',(0.,0.666550808889759,-0.745459602640149));
#18515=DIRECTION('ref_axis',(0.,0.745459602640149,0.666550808889759));
#18516=DIRECTION('center_axis',(0.,-0.666550808889759,0.745459602640149));
#18517=DIRECTION('ref_axis',(0.,-0.745459602640149,-0.666550808889759));
#18518=DIRECTION('',(0.,0.666550808889759,-0.745459602640149));
#18519=DIRECTION('center_axis',(0.,0.666550808889759,-0.745459602640149));
#18520=DIRECTION('ref_axis',(0.,-0.745459602640149,-0.666550808889759));
#18521=DIRECTION('center_axis',(-0.918412615811006,-0.26370342792269,0.294921632338166));
#18522=DIRECTION('ref_axis',(3.6676144219822E-17,0.745459602640148,0.66655080888976));
#18523=DIRECTION('center_axis',(1.,9.18849901475632E-33,8.21587303869647E-33));
#18524=DIRECTION('ref_axis',(5.20917225812029E-33,-0.919145030018058,0.393919298579167));
#18525=DIRECTION('center_axis',(-1.,1.34704820113771E-16,1.20445972511707E-16));
#18526=DIRECTION('ref_axis',(-1.63770145274277E-16,-0.393919298579167,-0.919145030018058));
#18527=DIRECTION('',(1.80700362080917E-16,0.745459602640149,0.666550808889759));
#18528=DIRECTION('',(1.80700362080917E-16,0.745459602640149,0.666550808889759));
#18529=DIRECTION('',(1.80700362080917E-16,0.745459602640149,0.666550808889759));
#18530=DIRECTION('center_axis',(1.,-2.15204789668062E-15,-1.92424815673669E-15));
#18531=DIRECTION('ref_axis',(-2.61639632775514E-15,-0.393919298579167,-0.919145030018058));
#18532=DIRECTION('',(2.88687393529957E-15,0.745459602640149,0.666550808889758));
#18533=DIRECTION('',(2.88687393529957E-15,0.745459602640149,0.666550808889758));
#18534=DIRECTION('center_axis',(-8.38164711797325E-31,0.666550808889758,
-0.745459602640149));
#18535=DIRECTION('ref_axis',(1.,-7.81247014752972E-31,-1.82290970109027E-30));
#18536=DIRECTION('center_axis',(2.48029812061751E-15,0.745459602640149,
0.666550808889758));
#18537=DIRECTION('ref_axis',(1.,-5.39435679172679E-15,2.31186719645433E-15));
#18538=DIRECTION('',(5.91645678915759E-31,-0.666550808889758,0.745459602640149));
#18539=DIRECTION('',(1.,-1.84896205142464E-15,-1.65324471858535E-15));
#18540=DIRECTION('',(5.91645678915759E-31,-0.666550808889758,0.745459602640149));
#18541=DIRECTION('',(-1.,1.84896205142464E-15,1.65324471858535E-15));
#18542=DIRECTION('center_axis',(4.95069485153125E-17,-0.745459602640149,
-0.666550808889758));
#18543=DIRECTION('ref_axis',(7.80070196304878E-34,-0.666550808889758,0.745459602640149));
#18544=DIRECTION('',(5.91645678915759E-31,-0.666550808889758,0.745459602640149));
#18545=DIRECTION('',(-1.,-3.69054301681519E-17,-3.29988965785444E-17));
#18546=DIRECTION('',(5.91645678915759E-31,-0.666550808889758,0.745459602640149));
#18547=DIRECTION('',(1.,3.69054301681518E-17,3.29988965785444E-17));
#18548=DIRECTION('center_axis',(-1.,3.2296864575908E-15,2.88781593683036E-15));
#18549=DIRECTION('ref_axis',(-3.92655748994937E-15,-0.393919298579167,-0.919145030018058));
#18550=DIRECTION('',(-4.33247683194691E-15,-0.745459602640149,-0.666550808889758));
#18551=DIRECTION('',(1.83098382774925E-15,-0.289055347086674,0.95731238700886));
#18552=DIRECTION('',(-4.33247683194691E-15,-0.745459602640149,-0.666550808889758));
#18553=DIRECTION('',(1.83098382774926E-15,0.919145030018058,-0.393919298579166));
#18554=DIRECTION('center_axis',(-4.48685329518507E-17,0.957312387008861,
0.289055347086674));
#18555=DIRECTION('ref_axis',(1.,2.74967668360758E-17,6.41591226175102E-17));
#18556=DIRECTION('',(-1.22004564440084E-15,0.289055347086674,-0.95731238700886));
#18557=DIRECTION('',(1.,3.69054301681519E-17,3.29988965785444E-17));
#18558=DIRECTION('center_axis',(-9.86076131526264E-31,0.666550808889758,
-0.745459602640149));
#18559=DIRECTION('ref_axis',(1.,-9.19114135003496E-31,-2.14459964834149E-30));
#18560=DIRECTION('',(2.88687393529957E-15,0.745459602640149,0.666550808889758));
#18561=DIRECTION('',(-1.,1.84896205142464E-15,1.65324471858535E-15));
#18562=DIRECTION('center_axis',(1.,-2.15204789668062E-15,-1.92424815673669E-15));
#18563=DIRECTION('ref_axis',(-2.61639632775514E-15,-0.393919298579167,-0.919145030018058));
#18564=DIRECTION('',(-1.22004564440084E-15,-0.919145030018058,0.393919298579166));
#18565=DIRECTION('',(2.88687393529957E-15,0.745459602640149,0.666550808889758));
#18566=DIRECTION('center_axis',(-6.73294499808336E-16,-0.745459602640149,
-0.666550808889758));
#18567=DIRECTION('ref_axis',(-4.59044537750992E-32,-0.666550808889758,0.745459602640149));
#18568=DIRECTION('',(5.91645678915759E-31,-0.666550808889758,0.745459602640149));
#18569=DIRECTION('',(1.,-5.01913850286919E-16,-4.48784993468272E-16));
#18570=DIRECTION('center_axis',(-1.,2.15204789668062E-15,1.92424815673669E-15));
#18571=DIRECTION('ref_axis',(-2.61639632775514E-15,-0.393919298579167,-0.919145030018058));
#18572=DIRECTION('',(-2.88687393529957E-15,-0.745459602640149,-0.666550808889758));
#18573=DIRECTION('center_axis',(-2.24791350088801E-15,-0.393919298579166,
-0.919145030018059));
#18574=DIRECTION('ref_axis',(-3.23063398772322E-32,-0.919145030018058,0.393919298579166));
#18575=DIRECTION('center_axis',(-6.16297582203916E-33,0.666550808889759,
-0.745459602640149));
#18576=DIRECTION('ref_axis',(1.,-5.74446334377187E-33,-1.34037478021344E-32));
#34475=CARTESIAN_POINT('',(0.,0.,0.));
#34476=CARTESIAN_POINT('Origin',(46.,34.999999994595,6.55002914876687E-10));
#34477=CARTESIAN_POINT('',(35.,38.8160931995804,8.90421747895505));
#34478=CARTESIAN_POINT('',(35.,42.2216398951714,6.45721096177453));
#34479=CARTESIAN_POINT('Origin',(35.,34.999999994595,6.55002914876687E-10));
#34480=CARTESIAN_POINT('',(35.,38.2526765117554,9.12511653277189));
#34481=CARTESIAN_POINT('Origin',(35.,34.999999994595,6.55002914876687E-10));
#34482=CARTESIAN_POINT('',(35.,27.7783600940186,-6.45721096046452));
#34483=CARTESIAN_POINT('Origin',(35.,34.999999994595,6.55002914876687E-10));
#34484=CARTESIAN_POINT('',(46.,27.7783600940186,-6.45721096046452));
#34485=CARTESIAN_POINT('',(46.,27.7783600940186,-6.45721096046452));
#34486=CARTESIAN_POINT('',(46.,42.2216398951714,6.45721096177453));
#34487=CARTESIAN_POINT('Origin',(46.,34.999999994595,6.55002914876687E-10));
#34488=CARTESIAN_POINT('',(46.,42.2216398951714,6.45721096177453));
#34489=CARTESIAN_POINT('Origin',(49.1839401118236,21.0000000000002,6.00000000000001));
#34490=CARTESIAN_POINT('',(33.,20.1857688098371,4.10012722295268));
#34491=CARTESIAN_POINT('Origin',(33.,21.0000000000002,6.00000000000001));
#34492=CARTESIAN_POINT('',(35.,20.1857688098371,4.10012722295268));
#34493=CARTESIAN_POINT('',(49.1839401118236,20.1857688098371,4.10012722295268));
#34494=CARTESIAN_POINT('Origin',(35.,21.0000000000002,6.00000000000001));
#34495=CARTESIAN_POINT('Origin',(33.,21.0000000000003,5.99999999999997));
#34496=CARTESIAN_POINT('',(28.,25.9586702584788,5.3584477669892));
#34497=CARTESIAN_POINT('',(28.,24.8843448987174,2.85168859421269));
#34498=CARTESIAN_POINT('Origin',(28.,21.0000000000003,5.99999999999997));
#34499=CARTESIAN_POINT('',(33.,25.9586702584788,5.3584477669892));
#34500=CARTESIAN_POINT('',(33.,25.9586702584788,5.3584477669892));
#34501=CARTESIAN_POINT('',(33.,24.8843448987174,2.85168859421269));
#34502=CARTESIAN_POINT('Origin',(33.,21.0000000000003,5.99999999999997));
#34503=CARTESIAN_POINT('',(33.,24.8843448987174,2.85168859421269));
#34504=CARTESIAN_POINT('Origin',(33.,35.0000000000003,1.87377939199425E-14));
#34505=CARTESIAN_POINT('',(28.,26.2716828895476,2.19464813110885));
#34506=CARTESIAN_POINT('',(28.,27.3912430012989,4.80695505852859));
#34507=CARTESIAN_POINT('Origin',(28.,35.0000000000003,1.87377939199425E-14));
#34508=CARTESIAN_POINT('',(33.,26.2716828895476,2.19464813110885));
#34509=CARTESIAN_POINT('',(33.,26.2716828895476,2.19464813110885));
#34510=CARTESIAN_POINT('',(33.,27.3912430012989,4.80695505852859));
#34511=CARTESIAN_POINT('Origin',(33.,35.0000000000003,1.87377939199425E-14));
#34512=CARTESIAN_POINT('',(33.,27.3912430012989,4.80695505852859));
#34513=CARTESIAN_POINT('Origin',(35.,36.2005438522226,0.262677966498032));
#34514=CARTESIAN_POINT('',(28.,39.4857043089188,8.64168272683559));
#34515=CARTESIAN_POINT('',(28.,44.4728491223851,-3.28259572071447));
#34516=CARTESIAN_POINT('Origin',(28.,36.2005438522226,0.262677966498032));
#34517=CARTESIAN_POINT('',(35.,39.4857043089188,8.64168272683559));
#34518=CARTESIAN_POINT('',(35.,39.4857043089188,8.64168272683559));
#34519=CARTESIAN_POINT('',(35.,44.3549070848781,4.07139957222298));
#34520=CARTESIAN_POINT('Origin',(35.,36.2005438522226,0.262677966498032));
#34521=CARTESIAN_POINT('',(35.,44.4728491223851,-3.28259572071447));
#34522=CARTESIAN_POINT('Origin',(35.,36.2005438522226,0.262677966498032));
#34523=CARTESIAN_POINT('',(35.,44.4728491223851,-3.28259572071447));
#34524=CARTESIAN_POINT('Origin',(36.5,49.8743530018414,-19.3357042103691));
#34525=CARTESIAN_POINT('',(36.5,44.5419465307234,-13.3720273892479));
#34526=CARTESIAN_POINT('',(36.,44.5419465307234,-13.3720273892479));
#34527=CARTESIAN_POINT('',(36.5,44.5419465307234,-13.3720273892479));
#34528=CARTESIAN_POINT('',(36.,49.8743530018414,-19.3357042103691));
#34529=CARTESIAN_POINT('',(36.,49.8743530018414,-19.3357042103691));
#34530=CARTESIAN_POINT('',(36.5,49.8743530018414,-19.3357042103691));
#34531=CARTESIAN_POINT('',(36.5,49.8743530018414,-19.3357042103691));
#34532=CARTESIAN_POINT('',(36.5,49.8743530018414,-19.3357042103691));
#34533=CARTESIAN_POINT('Origin',(36.5,50.0979908826335,-19.1357389677022));
#34534=CARTESIAN_POINT('',(36.5,44.7655844115154,-13.172062146581));
#34535=CARTESIAN_POINT('',(36.5,44.7655844115154,-13.172062146581));
#34536=CARTESIAN_POINT('',(36.5,50.0979908826335,-19.1357389677022));
#34537=CARTESIAN_POINT('',(36.5,50.0979908826335,-19.1357389677022));
#34538=CARTESIAN_POINT('',(36.5,50.0979908826335,-19.1357389677022));
#34539=CARTESIAN_POINT('Origin',(36.,50.0979908826335,-19.1357389677022));
#34540=CARTESIAN_POINT('',(36.,44.7655844115154,-13.172062146581));
#34541=CARTESIAN_POINT('',(36.,44.7655844115154,-13.172062146581));
#34542=CARTESIAN_POINT('',(36.,50.0979908826335,-19.1357389677022));
#34543=CARTESIAN_POINT('',(36.,50.0979908826335,-19.1357389677022));
#34544=CARTESIAN_POINT('',(36.,50.0979908826335,-19.1357389677022));
#34545=CARTESIAN_POINT('Origin',(28.,51.2161802865937,-18.1359127543675));
#34546=CARTESIAN_POINT('',(36.5,52.3343696905538,-17.1360865410329));
#34547=CARTESIAN_POINT('',(36.5,52.558007571346,-16.936121298366));
#34548=CARTESIAN_POINT('',(36.5,52.3343696905538,-17.1360865410329));
#34549=CARTESIAN_POINT('',(36.,52.3343696905538,-17.1360865410329));
#34550=CARTESIAN_POINT('',(36.,52.3343696905538,-17.1360865410329));
#34551=CARTESIAN_POINT('',(36.,52.558007571346,-16.936121298366));
#34552=CARTESIAN_POINT('',(36.,52.558007571346,-16.936121298366));
#34553=CARTESIAN_POINT('',(36.5,52.558007571346,-16.936121298366));
#34554=CARTESIAN_POINT('Origin',(36.,52.3343696905538,-17.1360865410329));
#34555=CARTESIAN_POINT('',(36.,47.0019632194358,-11.1724097199117));
#34556=CARTESIAN_POINT('',(36.5,47.0019632194358,-11.1724097199117));
#34557=CARTESIAN_POINT('',(36.,47.0019632194358,-11.1724097199117));
#34558=CARTESIAN_POINT('',(36.,52.3343696905538,-17.1360865410329));
#34559=CARTESIAN_POINT('',(36.5,52.3343696905538,-17.1360865410329));
#34560=CARTESIAN_POINT('Origin',(36.5,52.558007571346,-16.936121298366));
#34561=CARTESIAN_POINT('',(36.5,47.2256011002279,-10.9724444772448));
#34562=CARTESIAN_POINT('',(36.,47.2256011002279,-10.9724444772448));
#34563=CARTESIAN_POINT('',(36.5,47.2256011002279,-10.9724444772448));
#34564=CARTESIAN_POINT('',(36.5,52.558007571346,-16.936121298366));
#34565=CARTESIAN_POINT('',(36.,52.558007571346,-16.936121298366));
#34566=CARTESIAN_POINT('Origin',(28.,33.1363509879946,-1.66637702156941));
#34567=CARTESIAN_POINT('',(48.8,48.0194296622137,-18.3113705713116));
#34568=CARTESIAN_POINT('',(48.5,48.0194296622137,-18.3113705713116));
#34569=CARTESIAN_POINT('',(48.8,48.0194296622137,-18.3113705713116));
#34570=CARTESIAN_POINT('',(48.5,49.3656354031611,-19.8169452151862));
#34571=CARTESIAN_POINT('',(48.5,33.1363509879946,-1.66637702156941));
#34572=CARTESIAN_POINT('',(48.8,49.6858066844382,-20.175019577912));
#34573=CARTESIAN_POINT('',(48.,48.8320166010328,-19.2201546106433));
#34574=CARTESIAN_POINT('',(48.8,49.6858066844382,-20.175019577912));
#34575=CARTESIAN_POINT('Origin',(48.,48.0194296622137,-18.3113705713116));
#34576=CARTESIAN_POINT('',(48.,49.2047464023529,-18.8868792061983));
#34577=CARTESIAN_POINT('',(48.,52.1865848129134,-16.2206759706393));
#34578=CARTESIAN_POINT('',(48.,48.8320166010328,-19.2201546106433));
#34579=CARTESIAN_POINT('',(48.,48.3921594635339,-17.9780951668667));
#34580=CARTESIAN_POINT('',(48.,48.3921594635339,-17.9780951668667));
#34581=CARTESIAN_POINT('',(48.,51.3739978740944,-15.3118919313077));
#34582=CARTESIAN_POINT('',(48.,48.0194296622137,-18.3113705713116));
#34583=CARTESIAN_POINT('',(48.,52.1865848129134,-16.2206759706393));
#34584=CARTESIAN_POINT('Origin',(48.,48.8320166010328,-19.2201546106433));
#34585=CARTESIAN_POINT('',(39.9575325128956,46.6168572862855,-3.92682792990623));
#34586=CARTESIAN_POINT('',(48.5,53.0929334163619,-16.4841911707374));
#34587=CARTESIAN_POINT('',(47.57228567029,51.4112682420982,-15.9952575162825));
#34588=CARTESIAN_POINT('',(48.8,53.4131046976389,-16.8422655334632));
#34589=CARTESIAN_POINT('',(48.,52.5593146142335,-15.8874005661944));
#34590=CARTESIAN_POINT('',(48.8,49.6858066844382,-20.175019577912));
#34591=CARTESIAN_POINT('Origin',(28.,49.8830786688142,-16.6449935490872));
#34592=CARTESIAN_POINT('',(48.5,48.0194296622137,-18.3113705713116));
#34593=CARTESIAN_POINT('',(49.8,48.0194296622137,-18.3113705713116));
#34594=CARTESIAN_POINT('',(49.8,48.0194296622137,-18.3113705713116));
#34595=CARTESIAN_POINT('',(49.8,51.7467276754146,-14.9786165268629));
#34596=CARTESIAN_POINT('',(49.8,51.7467276754146,-14.9786165268629));
#34597=CARTESIAN_POINT('',(48.8,51.7467276754146,-14.9786165268629));
#34598=CARTESIAN_POINT('',(48.8,51.7467276754146,-14.9786165268629));
#34599=CARTESIAN_POINT('',(48.5,51.7467276754146,-14.9786165268629));
#34600=CARTESIAN_POINT('',(48.8,51.7467276754146,-14.9786165268629));
#34601=CARTESIAN_POINT('',(48.,51.3739978740944,-15.3118919313077));
#34602=CARTESIAN_POINT('Origin',(48.8,51.7467276754146,-14.9786165268629));
#34603=CARTESIAN_POINT('',(48.8,47.747422822076,-10.505858911022));
#34604=CARTESIAN_POINT('',(49.8,47.747422822076,-10.505858911022));
#34605=CARTESIAN_POINT('',(48.8,47.747422822076,-10.505858911022));
#34606=CARTESIAN_POINT('',(48.8,51.7467276754146,-14.9786165268629));
#34607=CARTESIAN_POINT('',(49.8,51.7467276754146,-14.9786165268629));
#34608=CARTESIAN_POINT('Origin',(49.8,48.0194296622137,-18.3113705713116));
#34609=CARTESIAN_POINT('',(49.8,44.0201248088753,-13.8386129554708));
#34610=CARTESIAN_POINT('',(48.8,44.0201248088753,-13.8386129554708));
#34611=CARTESIAN_POINT('',(49.8,44.0201248088753,-13.8386129554708));
#34612=CARTESIAN_POINT('',(49.8,48.0194296622137,-18.3113705713116));
#34613=CARTESIAN_POINT('',(48.8,48.0194296622137,-18.3113705713116));
#34614=CARTESIAN_POINT('Origin',(48.8,61.4283911851505,-9.67541749392847));
#34615=CARTESIAN_POINT('',(49.8,48.1486287370291,-21.5494833323853));
#34616=CARTESIAN_POINT('',(48.8,46.8574548302663,-22.7039831992086));
#34617=CARTESIAN_POINT('Origin',(47.8,48.1486287370291,-21.5494833323853));
#34618=CARTESIAN_POINT('',(48.8,48.5676172804779,-21.1748457912466));
#34619=CARTESIAN_POINT('',(48.8,61.4283911851505,-9.67541749392847));
#34620=CARTESIAN_POINT('',(48.8,61.4283911851505,-9.67541749392847));
#34621=CARTESIAN_POINT('',(48.8,54.5312941015992,-15.8424393201286));
#34622=CARTESIAN_POINT('',(48.8,61.4283911851505,-9.67541749392847));
#34623=CARTESIAN_POINT('',(48.8,56.2414565518108,-14.3133019121667));
#34624=CARTESIAN_POINT('',(48.8,61.4283911851505,-9.67541749392847));
#34625=CARTESIAN_POINT('',(49.8,54.950282645048,-15.4678017789899));
#34626=CARTESIAN_POINT('Origin',(47.8,54.950282645048,-15.4678017789899));
#34627=CARTESIAN_POINT('',(49.8,61.4283911851505,-9.67541749392847));
#34628=CARTESIAN_POINT('Origin',(46.,65.7609714429338,-14.5209049110894));
#34629=CARTESIAN_POINT('',(48.2499021086877,47.5471157171578,-23.8003792172667));
#34630=CARTESIAN_POINT('',(46.,50.6412872520117,-28.0401320991545));
#34631=CARTESIAN_POINT('',(45.1007678884438,51.8779536794353,-29.7346600173847));
#34632=CARTESIAN_POINT('',(46.,52.3038298561492,-26.5535738555194));
#34633=CARTESIAN_POINT('',(46.,65.7609714429338,-14.5209049110894));
#34634=CARTESIAN_POINT('',(48.,49.2091296720183,-23.0925114146902));
#34635=CARTESIAN_POINT('',(51.3562786983429,44.0157915191397,-17.2843663427951));
#34636=CARTESIAN_POINT('Origin',(47.9999999999999,49.8054973541307,-22.5592707675784));
#34637=CARTESIAN_POINT('Origin',(47.800000000136,49.6959788286485,-23.2800145527791));
#34638=CARTESIAN_POINT('Origin',(46.,53.1054137160521,-5.71502497212683));
#34639=CARTESIAN_POINT('',(42.,39.2212286168793,-18.1295337876985));
#34640=CARTESIAN_POINT('',(40.5,39.2212286168793,-18.1295337876985));
#34641=CARTESIAN_POINT('',(42.,39.2212286168793,-18.1295337876985));
#34642=CARTESIAN_POINT('',(40.5,39.6964591135624,-17.7046076470313));
#34643=CARTESIAN_POINT('',(40.5,38.9509995109222,-18.3711584559211));
#34644=CARTESIAN_POINT('',(46.,40.6430251186653,-16.8582380595522));
#34645=CARTESIAN_POINT('',(40.5,39.6964591135624,-17.7046076470313));
#34646=CARTESIAN_POINT('',(46.,38.6621339148992,-18.6294468943659));
#34647=CARTESIAN_POINT('',(46.,53.1054137160521,-5.71502497212683));
#34648=CARTESIAN_POINT('',(42.,38.6621339148992,-18.6294468943659));
#34649=CARTESIAN_POINT('',(46.,38.6621339148992,-18.6294468943659));
#34650=CARTESIAN_POINT('',(42.,39.2212286168793,-18.1295337876985));
#34651=CARTESIAN_POINT('Origin',(40.35,49.3810785931525,-22.4596728974293));
#34652=CARTESIAN_POINT('',(40.35,49.5609187050531,-20.8604902883506));
#34653=CARTESIAN_POINT('',(40.35,43.6101220274232,-14.2052159003601));
#34654=CARTESIAN_POINT('',(40.35,50.2756301163208,-21.6598119267616));
#34655=CARTESIAN_POINT('',(40.35,49.9029003150007,-21.9930873312064));
#34656=CARTESIAN_POINT('',(40.35,49.9029003150006,-21.9930873312065));
#34657=CARTESIAN_POINT('',(40.35,49.7538083944726,-22.1263974929844));
#34658=CARTESIAN_POINT('',(40.35,49.3810785931525,-22.4596728974293));
#34659=CARTESIAN_POINT('',(40.35,48.6663671818848,-21.6603512590183));
#34660=CARTESIAN_POINT('',(40.35,49.7538083944726,-22.1263974929844));
#34661=CARTESIAN_POINT('',(40.35,42.7155705042549,-15.0050768710278));
#34662=CARTESIAN_POINT('',(40.35,49.3810785931525,-22.4596728974293));
#34663=CARTESIAN_POINT('',(40.35,42.7155705042549,-15.0050768710278));
#34664=CARTESIAN_POINT('Origin',(40.65,49.3810785931525,-22.4596728974293));
#34665=CARTESIAN_POINT('',(40.65,48.6663671818848,-21.6603512590183));
#34666=CARTESIAN_POINT('',(40.65,48.6663671818848,-21.6603512590183));
#34667=CARTESIAN_POINT('',(40.65,42.7155705042549,-15.0050768710278));
#34668=CARTESIAN_POINT('',(40.65,49.3810785931525,-22.4596728974293));
#34669=CARTESIAN_POINT('',(40.65,42.7155705042549,-15.0050768710278));
#34670=CARTESIAN_POINT('Origin',(40.65,54.8229336924257,-17.5938519925341));
#34671=CARTESIAN_POINT('',(40.35,54.1082222811579,-16.794530354123));
#34672=CARTESIAN_POINT('',(40.35,48.1574256035281,-10.1392559661326));
#34673=CARTESIAN_POINT('',(40.35,54.8229336924257,-17.5938519925341));
#34674=CARTESIAN_POINT('',(40.65,54.1082222811579,-16.794530354123));
#34675=CARTESIAN_POINT('',(40.65,54.1082222811579,-16.794530354123));
#34676=CARTESIAN_POINT('',(40.65,48.1574256035281,-10.1392559661326));
#34677=CARTESIAN_POINT('',(40.65,54.8229336924257,-17.5938519925341));
#34678=CARTESIAN_POINT('',(40.65,48.1574256035281,-10.1392559661326));
#34679=CARTESIAN_POINT('Origin',(40.65,55.7174852155938,-16.7939910218664));
#34680=CARTESIAN_POINT('',(40.65,55.3447554142738,-17.1272664263113));
#34681=CARTESIAN_POINT('',(40.65,55.1956634937457,-17.2605765880892));
#34682=CARTESIAN_POINT('',(40.65,55.7174852155938,-16.7939910218664));
#34683=CARTESIAN_POINT('',(40.65,55.0027738043262,-15.9946693834553));
#34684=CARTESIAN_POINT('',(40.65,55.3447554142738,-17.1272664263113));
#34685=CARTESIAN_POINT('',(40.65,49.0519771266963,-9.33939499546487));
#34686=CARTESIAN_POINT('',(40.65,55.7174852155938,-16.7939910218664));
#34687=CARTESIAN_POINT('',(40.65,49.0519771266963,-9.33939499546487));
#34688=CARTESIAN_POINT('',(40.65,55.1956634937457,-17.2605765880892));
#34689=CARTESIAN_POINT('Origin',(28.,49.7538083944727,-22.1263974929844));
#34690=CARTESIAN_POINT('',(40.65,49.7538083944726,-22.1263974929844));
#34691=CARTESIAN_POINT('',(40.65,49.7538083944726,-22.1263974929844));
#34692=CARTESIAN_POINT('',(40.35,49.7538083944726,-22.1263974929844));
#34693=CARTESIAN_POINT('Origin',(28.,49.9029003150007,-21.9930873312064));
#34694=CARTESIAN_POINT('',(40.65,49.5609187050531,-20.8604902883506));
#34695=CARTESIAN_POINT('',(40.35,49.5609187050531,-20.8604902883506));
#34696=CARTESIAN_POINT('',(40.65,49.9029003150007,-21.9930873312064));
#34697=CARTESIAN_POINT('',(40.65,49.9029003150006,-21.9930873312065));
#34698=CARTESIAN_POINT('',(40.65,49.9029003150007,-21.9930873312064));
#34699=CARTESIAN_POINT('Origin',(28.,52.5492819043732,-19.6268319596478));
#34700=CARTESIAN_POINT('',(40.65,50.2756301163208,-21.6598119267616));
#34701=CARTESIAN_POINT('Origin',(28.,55.1956634937457,-17.2605765880892));
#34702=CARTESIAN_POINT('',(40.35,55.1956634937457,-17.2605765880892));
#34703=CARTESIAN_POINT('',(40.35,55.1956634937457,-17.2605765880892));
#34704=CARTESIAN_POINT('',(40.35,55.1956634937457,-17.2605765880892));
#34705=CARTESIAN_POINT('Origin',(28.,55.3447554142738,-17.1272664263113));
#34706=CARTESIAN_POINT('',(40.35,55.0027738043262,-15.9946693834553));
#34707=CARTESIAN_POINT('',(40.35,55.3447554142738,-17.1272664263113));
#34708=CARTESIAN_POINT('',(40.35,55.3447554142738,-17.1272664263113));
#34709=CARTESIAN_POINT('',(40.35,55.0027738043262,-15.9946693834553));
#34710=CARTESIAN_POINT('',(40.65,55.3447554142738,-17.1272664263113));
#34711=CARTESIAN_POINT('Origin',(28.,51.2161802865937,-18.1359127543675));
#34712=CARTESIAN_POINT('',(36.,49.8743530018414,-19.3357042103691));
#34713=CARTESIAN_POINT('Origin',(38.5,58.3261827962024,-18.886372642664));
#34714=CARTESIAN_POINT('',(35.7,59.4602420414948,-20.1546860901778));
#34715=CARTESIAN_POINT('',(36.,58.3261827962024,-18.886372642664));
#34716=CARTESIAN_POINT('',(35.7,59.4602420414948,-20.1546860901778));
#34717=CARTESIAN_POINT('',(38.5,61.5475289288871,-18.2883438252864));
#34718=CARTESIAN_POINT('Origin',(38.5,59.4602420414948,-20.1546860901778));
#34719=CARTESIAN_POINT('',(38.5,60.1898318028027,-17.2199956204396));
#34720=CARTESIAN_POINT('',(38.5,60.1898318028027,-17.2199956204396));
#34721=CARTESIAN_POINT('Origin',(38.5,58.3261827962024,-18.886372642664));
#34722=CARTESIAN_POINT('Origin',(42.5,60.1898318028026,-17.2199956204395));
#34723=CARTESIAN_POINT('',(42.5,61.5475289288871,-18.2883438252864));
#34724=CARTESIAN_POINT('',(38.5,61.5475289288871,-18.2883438252864));
#34725=CARTESIAN_POINT('',(42.5,60.1898318028026,-17.2199956204395));
#34726=CARTESIAN_POINT('',(42.5,60.1898318028026,-17.2199956204395));
#34727=CARTESIAN_POINT('',(42.5,60.1898318028026,-17.2199956204395));
#34728=CARTESIAN_POINT('Origin',(36.,58.3261827962024,-18.886372642664));
#34729=CARTESIAN_POINT('',(36.,51.1697706108569,-25.2852604080056));
#34730=CARTESIAN_POINT('',(36.,58.3261827962024,-18.886372642664));
#34731=CARTESIAN_POINT('',(35.7,52.3038298561492,-26.5535738555194));
#34732=CARTESIAN_POINT('',(35.7,52.3038298561492,-26.5535738555194));
#34733=CARTESIAN_POINT('',(35.7,59.4602420414948,-20.1546860901778));
#34734=CARTESIAN_POINT('Origin',(42.5,58.3261827962024,-18.886372642664));
#34735=CARTESIAN_POINT('',(45.3,59.4602420414948,-20.1546860901778));
#34736=CARTESIAN_POINT('Origin',(42.5,59.4602420414948,-20.1546860901778));
#34737=CARTESIAN_POINT('',(45.,58.3261827962023,-18.886372642664));
#34738=CARTESIAN_POINT('',(45.,58.3261827962023,-18.886372642664));
#34739=CARTESIAN_POINT('Origin',(42.5,58.3261827962024,-18.886372642664));
#34740=CARTESIAN_POINT('Origin',(38.5,51.1697706108569,-25.2852604080056));
#34741=CARTESIAN_POINT('',(38.5,49.3061216042565,-26.95163743023));
#34742=CARTESIAN_POINT('Origin',(38.5,51.1697706108569,-25.2852604080056));
#34743=CARTESIAN_POINT('',(38.5,50.2165429687568,-28.4199161204107));
#34744=CARTESIAN_POINT('',(38.5,50.2165429687568,-28.4199161204107));
#34745=CARTESIAN_POINT('Origin',(38.5,52.3038298561492,-26.5535738555194));
#34746=CARTESIAN_POINT('Origin',(45.,58.3261827962023,-18.886372642664));
#34747=CARTESIAN_POINT('',(45.3,52.3038298561492,-26.5535738555194));
#34748=CARTESIAN_POINT('',(45.3,59.4602420414947,-20.1546860901777));
#34749=CARTESIAN_POINT('',(45.,51.1697706108569,-25.2852604080056));
#34750=CARTESIAN_POINT('',(45.,51.1697706108569,-25.2852604080056));
#34751=CARTESIAN_POINT('',(45.,58.3261827962023,-18.886372642664));
#34752=CARTESIAN_POINT('Origin',(42.5,49.3061216042565,-26.9516374302301));
#34753=CARTESIAN_POINT('',(42.5,49.3061216042565,-26.9516374302301));
#34754=CARTESIAN_POINT('',(42.5,49.3061216042565,-26.9516374302301));
#34755=CARTESIAN_POINT('',(42.5,50.2165429687568,-28.4199161204107));
#34756=CARTESIAN_POINT('',(42.5,50.2165429687568,-28.4199161204107));
#34757=CARTESIAN_POINT('',(38.5,50.2165429687568,-28.4199161204107));
#34758=CARTESIAN_POINT('Origin',(40.35,55.7174852155938,-16.7939910218664));
#34759=CARTESIAN_POINT('',(40.35,49.0519771266963,-9.33939499546487));
#34760=CARTESIAN_POINT('',(40.35,55.7174852155938,-16.7939910218664));
#34761=CARTESIAN_POINT('',(40.35,49.0519771266963,-9.33939499546487));
#34762=CARTESIAN_POINT('Origin',(42.5,51.1697706108569,-25.2852604080056));
#34763=CARTESIAN_POINT('Origin',(42.5,52.3038298561492,-26.5535738555194));
#34764=CARTESIAN_POINT('Origin',(42.5,51.1697706108569,-25.2852604080056));
#34765=CARTESIAN_POINT('Origin',(36.5,52.3343696905538,-17.1360865410329));
#34766=CARTESIAN_POINT('',(36.5,47.0019632194358,-11.1724097199117));
#34767=CARTESIAN_POINT('Origin',(28.,36.8636490011954,1.66637702287939));
#34768=CARTESIAN_POINT('',(48.5,51.7467276754146,-14.9786165268629));
#34769=CARTESIAN_POINT('',(48.8,53.4131046976389,-16.8422655334632));
#34770=CARTESIAN_POINT('Origin',(48.,51.3739978740944,-15.3118919313077));
#34771=CARTESIAN_POINT('Origin',(48.5,33.1363509879946,-1.66637702156941));
#34772=CARTESIAN_POINT('Origin',(35.,26.4453341955376,13.754426956311));
#34773=CARTESIAN_POINT('',(28.,26.4453341955376,13.754426956311));
#34774=CARTESIAN_POINT('',(28.,26.4453341955376,13.754426956311));
#34775=CARTESIAN_POINT('',(35.,26.4453341955376,13.754426956311));
#34776=CARTESIAN_POINT('',(35.,26.4453341955376,13.754426956311));
#34777=CARTESIAN_POINT('',(35.,26.4453341955376,13.754426956311));
#34778=CARTESIAN_POINT('',(35.,26.4453341955376,13.754426956311));
#34779=CARTESIAN_POINT('',(35.,26.4453341955376,13.754426956311));
#34780=CARTESIAN_POINT('Origin',(35.,43.9100514671661,-4.59579024955887));
#34781=CARTESIAN_POINT('',(28.,43.9100514671661,-4.59579024955887));
#34782=CARTESIAN_POINT('',(28.,43.9100514671661,-4.59579024955887));
#34783=CARTESIAN_POINT('',(35.,43.9100514671661,-4.59579024955887));
#34784=CARTESIAN_POINT('',(35.,43.9100514671661,-4.59579024955887));
#34785=CARTESIAN_POINT('',(35.,43.9100514671661,-4.59579024955887));
#34786=CARTESIAN_POINT('Origin',(35.,35.6377461970035,-1.05051656234637));
#34787=CARTESIAN_POINT('',(28.,31.8358189268944,-9.20804983122126));
#34788=CARTESIAN_POINT('Origin',(28.,35.6377461970035,-1.05051656234637));
#34789=CARTESIAN_POINT('',(35.,31.8358189268944,-9.20804983122126));
#34790=CARTESIAN_POINT('Origin',(35.,35.6377461970035,-1.05051656234637));
#34791=CARTESIAN_POINT('',(35.,31.8358189268944,-9.20804983122126));
#34792=CARTESIAN_POINT('Origin',(35.,19.14012819977,-3.29105370048002));
#34793=CARTESIAN_POINT('',(28.,19.14012819977,-3.29105370048002));
#34794=CARTESIAN_POINT('',(28.,19.14012819977,-3.29105370048002));
#34795=CARTESIAN_POINT('',(35.,29.0964332376969,-7.93132256431019));
#34796=CARTESIAN_POINT('',(35.,19.14012819977,-3.29105370048002));
#34797=CARTESIAN_POINT('',(35.,19.14012819977,-3.29105370048002));
#34798=CARTESIAN_POINT('',(35.,19.14012819977,-3.29105370048002));
#34799=CARTESIAN_POINT('',(35.,19.14012819977,-3.29105370048002));
#34800=CARTESIAN_POINT('Origin',(35.,22.9420554698791,4.86647956839487));
#34801=CARTESIAN_POINT('',(28.,14.6697501997166,8.41175325560737));
#34802=CARTESIAN_POINT('Origin',(28.,22.9420554698791,4.86647956839487));
#34803=CARTESIAN_POINT('',(35.,14.6697501997166,8.41175325560737));
#34804=CARTESIAN_POINT('Origin',(35.,22.9420554698791,4.86647956839487));
#34805=CARTESIAN_POINT('',(35.,14.6697501997166,8.41175325560737));
#34806=CARTESIAN_POINT('Origin',(35.,23.1601737388414,5.37542219597347));
#34807=CARTESIAN_POINT('',(28.,14.8878684686789,8.92069588318597));
#34808=CARTESIAN_POINT('Origin',(28.,23.1601737388414,5.37542219597347));
#34809=CARTESIAN_POINT('',(35.,14.8878684686789,8.92069588318597));
#34810=CARTESIAN_POINT('',(35.,14.8878684686789,8.92069588318597));
#34811=CARTESIAN_POINT('Origin',(35.,23.1601737388414,5.37542219597347));
#34812=CARTESIAN_POINT('Origin',(35.,14.8878684686789,8.92069588318597));
#34813=CARTESIAN_POINT('',(28.,14.8878684686789,8.92069588318597));
#34814=CARTESIAN_POINT('',(35.,14.8878684686789,8.92069588318597));
#34815=CARTESIAN_POINT('Origin',(33.,25.7867763834114,2.31657302728156));
#34816=CARTESIAN_POINT('',(28.,25.9837360327009,2.77614554229058));
#34817=CARTESIAN_POINT('Origin',(28.,25.7867763834114,2.31657302728156));
#34818=CARTESIAN_POINT('',(33.,25.9837360327009,2.77614554229058));
#34819=CARTESIAN_POINT('',(33.,25.9837360327009,2.77614554229058));
#34820=CARTESIAN_POINT('Origin',(33.,25.7867763834114,2.31657302728156));
#34821=CARTESIAN_POINT('Origin',(33.,26.9685342791489,5.07400811733573));
#34822=CARTESIAN_POINT('',(28.,26.7715746298593,4.6144356023267));
#34823=CARTESIAN_POINT('Origin',(28.,26.9685342791489,5.07400811733573));
#34824=CARTESIAN_POINT('',(33.,26.7715746298593,4.6144356023267));
#34825=CARTESIAN_POINT('Origin',(33.,26.9685342791489,5.07400811733573));
#34826=CARTESIAN_POINT('',(33.,26.7715746298593,4.6144356023267));
#34827=CARTESIAN_POINT('Origin',(33.,26.257577635037,4.83472002867911));
#34828=CARTESIAN_POINT('',(28.,26.257577635037,4.83472002867911));
#34829=CARTESIAN_POINT('',(28.,26.257577635037,4.83472002867911));
#34830=CARTESIAN_POINT('',(33.,26.257577635037,4.83472002867911));
#34831=CARTESIAN_POINT('',(33.,26.257577635037,4.83472002867911));
#34832=CARTESIAN_POINT('',(33.,26.257577635037,4.83472002867911));
#34833=CARTESIAN_POINT('Origin',(33.,26.4545372843266,5.29429254368814));
#34834=CARTESIAN_POINT('Origin',(28.,26.4545372843266,5.29429254368814));
#34835=CARTESIAN_POINT('Origin',(33.,26.4545372843266,5.29429254368814));
#34836=CARTESIAN_POINT('Origin',(33.,25.2727793885891,2.53685745363396));
#34837=CARTESIAN_POINT('',(28.,25.4697390378787,2.99642996864299));
#34838=CARTESIAN_POINT('Origin',(28.,25.2727793885891,2.53685745363396));
#34839=CARTESIAN_POINT('',(33.,25.4697390378787,2.99642996864299));
#34840=CARTESIAN_POINT('Origin',(33.,25.2727793885891,2.53685745363396));
#34841=CARTESIAN_POINT('',(33.,25.4697390378787,2.99642996864299));
#34842=CARTESIAN_POINT('Origin',(35.,23.1601737388414,5.37542219597347));
#34843=CARTESIAN_POINT('',(35.,42.2216398951714,6.45721096177453));
#34844=CARTESIAN_POINT('Origin',(28.,23.1601737388414,5.37542219597347));
#34845=CARTESIAN_POINT('',(28.,25.4697390378787,2.99642996864299));
#34846=CARTESIAN_POINT('Origin',(33.,25.7867763834114,2.31657302728156));
#34847=CARTESIAN_POINT('',(33.,25.4697390378787,2.99642996864299));
#34848=CARTESIAN_POINT('Origin',(33.,25.4697390378787,2.99642996864299));
#34849=CARTESIAN_POINT('Origin',(46.,53.1054137160521,-5.71502497212683));
#34850=CARTESIAN_POINT('',(35.,42.3055677228029,-15.3716798159172));
#34851=CARTESIAN_POINT('',(35.,39.2212286168793,-18.1295337876985));
#34852=CARTESIAN_POINT('',(35.,53.1054137160521,-5.71502497212683));
#34853=CARTESIAN_POINT('',(38.5,39.6964591135624,-17.7046076470313));
#34854=CARTESIAN_POINT('Origin',(38.5,42.3055677228029,-15.3716798159172));
#34855=CARTESIAN_POINT('',(39.7,39.6964591135624,-17.7046076470313));
#34856=CARTESIAN_POINT('',(39.7,39.6964591135624,-17.7046076470313));
#34857=CARTESIAN_POINT('',(39.7,39.2212286168793,-18.1295337876985));
#34858=CARTESIAN_POINT('',(39.7,38.9509995109222,-18.3711584559211));
#34859=CARTESIAN_POINT('',(42.,39.2212286168793,-18.1295337876985));
#34860=CARTESIAN_POINT('Origin',(35.,23.1601737388414,5.37542219597347));
#34861=CARTESIAN_POINT('',(35.,27.7783600940186,-6.45721096046452));
#34862=CARTESIAN_POINT('Origin',(46.,42.2216398951714,6.45721096177453));
#34863=CARTESIAN_POINT('',(42.,49.7726596716033,-1.98772695892608));
#34864=CARTESIAN_POINT('',(42.,53.1054137160521,-5.71502497212683));
#34865=CARTESIAN_POINT('',(42.,49.7726596716033,-1.98772695892608));
#34866=CARTESIAN_POINT('',(41.,49.1061088627135,-1.24226735628591));
#34867=CARTESIAN_POINT('',(41.,49.1061088627135,-1.24226735628591));
#34868=CARTESIAN_POINT('',(35.,49.1061088627135,-1.24226735628591));
#34869=CARTESIAN_POINT('',(35.,49.1061088627135,-1.24226735628591));
#34870=CARTESIAN_POINT('',(35.,42.2216398951714,6.45721096177453));
#34871=CARTESIAN_POINT('',(46.,53.1054137160521,-5.71502497212683));
#34872=CARTESIAN_POINT('',(46.,42.2216398951714,6.45721096177453));
#34873=CARTESIAN_POINT('',(46.,53.1054137160521,-5.71502497212683));
#34874=CARTESIAN_POINT('Origin',(35.,34.999999994595,6.55002914876687E-10));
#34875=CARTESIAN_POINT('Origin',(46.,53.1054137160521,-5.71502497212683));
#34876=CARTESIAN_POINT('',(46.,51.124522512286,-7.4862338069405));
#34877=CARTESIAN_POINT('',(40.5,52.0710885173889,-6.63986421946138));
#34878=CARTESIAN_POINT('',(40.5,52.0710885173889,-6.63986421946138));
#34879=CARTESIAN_POINT('',(40.5,52.5463190140719,-6.21493807879413));
#34880=CARTESIAN_POINT('',(40.5,52.0710885173889,-6.63986421946138));
#34881=CARTESIAN_POINT('',(42.,52.5463190140719,-6.21493807879413));
#34882=CARTESIAN_POINT('',(42.,52.5463190140719,-6.21493807879413));
#34883=CARTESIAN_POINT('',(42.,52.5463190140719,-6.21493807879413));
#34884=CARTESIAN_POINT('',(46.,53.1054137160521,-5.71502497212683));
#34885=CARTESIAN_POINT('Origin',(46.,27.7783600940186,-6.45721096046452));
#34886=CARTESIAN_POINT('',(41.,34.6628290615606,-14.156689278525));
#34887=CARTESIAN_POINT('',(42.,35.3293798704504,-14.9021488811651));
#34888=CARTESIAN_POINT('',(41.,34.6628290615606,-14.156689278525));
#34889=CARTESIAN_POINT('',(42.,35.3293798704504,-14.9021488811651));
#34890=CARTESIAN_POINT('',(46.,27.7783600940186,-6.45721096046452));
#34891=CARTESIAN_POINT('',(35.,34.6628290615606,-14.156689278525));
#34892=CARTESIAN_POINT('',(35.,27.7783600940186,-6.45721096046452));
#34893=CARTESIAN_POINT('',(35.,34.6628290615606,-14.156689278525));
#34894=CARTESIAN_POINT('Origin',(35.,34.999999994595,6.55002914876687E-10));
#34895=CARTESIAN_POINT('',(35.,48.5470141607334,-1.74218046295324));
#34896=CARTESIAN_POINT('',(35.,48.5470141607334,-1.74218046295324));
#34897=CARTESIAN_POINT('',(35.,52.5463190140719,-6.21493807879413));
#34898=CARTESIAN_POINT('',(35.,52.5463190140719,-6.21493807879413));
#34899=CARTESIAN_POINT('',(35.,49.4619799081484,-8.97279205057551));
#34900=CARTESIAN_POINT('',(35.,53.1054137160521,-5.71502497212683));
#34901=CARTESIAN_POINT('',(35.,59.4602420414948,-20.1546860901778));
#34902=CARTESIAN_POINT('',(35.,59.4602420414948,-20.1546860901778));
#34903=CARTESIAN_POINT('',(35.,52.3038298561492,-26.5535738555194));
#34904=CARTESIAN_POINT('',(35.,52.3038298561492,-26.5535738555194));
#34905=CARTESIAN_POINT('',(35.,52.3038298561492,-26.5535738555194));
#34906=CARTESIAN_POINT('',(35.,35.2219237635407,-13.6567761718577));
#34907=CARTESIAN_POINT('',(35.,39.2212286168793,-18.1295337876985));
#34908=CARTESIAN_POINT('',(35.,35.2219237635407,-13.6567761718577));
#34909=CARTESIAN_POINT('Origin',(46.,34.999999994595,6.55002914876687E-10));
#34910=CARTESIAN_POINT('',(46.,42.3055677228029,-15.3716798159172));
#34911=CARTESIAN_POINT('',(46.,53.1054137160521,-5.71502497212683));
#34912=CARTESIAN_POINT('',(46.,49.4619799081483,-8.97279205057553));
#34913=CARTESIAN_POINT('',(46.,53.1054137160521,-5.71502497212683));
#34914=CARTESIAN_POINT('',(46.,53.1054137160521,-5.71502497212683));
#34915=CARTESIAN_POINT('Origin',(41.,35.2219237635407,-13.6567761718577));
#34916=CARTESIAN_POINT('',(41.,35.2219237635407,-13.6567761718577));
#34917=CARTESIAN_POINT('',(41.,35.2219237635407,-13.6567761718577));
#34918=CARTESIAN_POINT('',(42.,35.8884745724305,-14.4022357744978));
#34919=CARTESIAN_POINT('',(41.,35.2219237635407,-13.6567761718577));
#34920=CARTESIAN_POINT('',(42.,35.8884745724305,-14.4022357744978));
#34921=CARTESIAN_POINT('Origin',(42.,35.8884745724305,-14.4022357744978));
#34922=CARTESIAN_POINT('',(42.,35.8884745724305,-14.4022357744978));
#34923=CARTESIAN_POINT('Origin',(35.,35.2219237635407,-13.6567761718577));
#34924=CARTESIAN_POINT('',(35.,35.2219237635407,-13.6567761718577));
#34925=CARTESIAN_POINT('Origin',(28.,28.3374547959987,-5.9572978537972));
#34926=CARTESIAN_POINT('',(42.,39.2212286168793,-18.1295337876985));
#34927=CARTESIAN_POINT('Origin',(41.,48.5470141607334,-1.74218046295324));
#34928=CARTESIAN_POINT('',(42.,49.2135649696232,-2.48764006559341));
#34929=CARTESIAN_POINT('',(42.,49.2135649696232,-2.48764006559341));
#34930=CARTESIAN_POINT('',(41.,48.5470141607334,-1.74218046295324));
#34931=CARTESIAN_POINT('',(41.,48.5470141607334,-1.74218046295324));
#34932=CARTESIAN_POINT('',(41.,48.5470141607334,-1.74218046295324));
#34933=CARTESIAN_POINT('Origin',(42.,49.2135649696232,-2.48764006559341));
#34934=CARTESIAN_POINT('',(42.,49.2135649696232,-2.48764006559341));
#34935=CARTESIAN_POINT('Origin',(35.,48.5470141607334,-1.74218046295324));
#34936=CARTESIAN_POINT('',(35.,48.5470141607334,-1.74218046295324));
#34937=CARTESIAN_POINT('Origin',(28.,41.6625451931913,5.95729785510721));
#34938=CARTESIAN_POINT('',(39.7,52.5463190140719,-6.21493807879413));
#34939=CARTESIAN_POINT('',(42.,52.5463190140719,-6.21493807879413));
#34940=CARTESIAN_POINT('',(42.,52.5463190140719,-6.21493807879413));
#34941=CARTESIAN_POINT('Origin',(40.5,62.0693506507352,-17.8217582590636));
#34942=CARTESIAN_POINT('',(40.5,62.0693506507352,-17.8217582590636));
#34943=CARTESIAN_POINT('',(40.5,62.0693506507352,-17.8217582590636));
#34944=CARTESIAN_POINT('',(40.5,62.8148102533754,-17.1552074501738));
#34945=CARTESIAN_POINT('',(40.5,62.0693506507352,-17.8217582590636));
#34946=CARTESIAN_POINT('',(40.5,52.8165481200291,-5.97331341057162));
#34947=CARTESIAN_POINT('',(40.5,62.8148102533754,-17.1552074501738));
#34948=CARTESIAN_POINT('',(40.5,52.0710885173889,-6.63986421946138));
#34949=CARTESIAN_POINT('Origin',(40.5,62.8148102533754,-17.1552074501738));
#34950=CARTESIAN_POINT('',(39.7,52.8165481200291,-5.97331341057162));
#34951=CARTESIAN_POINT('',(40.5,52.8165481200291,-5.97331341057162));
#34952=CARTESIAN_POINT('',(39.7,62.8148102533754,-17.1552074501738));
#34953=CARTESIAN_POINT('',(40.5,62.8148102533754,-17.1552074501738));
#34954=CARTESIAN_POINT('',(39.7,62.8148102533754,-17.1552074501738));
#34955=CARTESIAN_POINT('Origin',(39.7,62.8148102533754,-17.1552074501738));
#34956=CARTESIAN_POINT('',(39.7,52.8165481200291,-5.97331341057162));
#34957=CARTESIAN_POINT('',(39.7,62.0693506507352,-17.8217582590636));
#34958=CARTESIAN_POINT('',(39.7,62.8148102533754,-17.1552074501738));
#34959=CARTESIAN_POINT('',(39.7,52.0710885173889,-6.63986421946138));
#34960=CARTESIAN_POINT('',(39.7,62.0693506507352,-17.8217582590636));
#34961=CARTESIAN_POINT('',(39.7,52.8165481200291,-5.97331341057162));
#34962=CARTESIAN_POINT('Origin',(38.5,62.0693506507352,-17.8217582590636));
#34963=CARTESIAN_POINT('',(38.5,52.0710885173889,-6.63986421946138));
#34964=CARTESIAN_POINT('',(38.5,52.0710885173889,-6.63986421946138));
#34965=CARTESIAN_POINT('',(38.5,62.0693506507352,-17.8217582590636));
#34966=CARTESIAN_POINT('',(38.5,62.0693506507352,-17.8217582590636));
#34967=CARTESIAN_POINT('',(38.5,62.0693506507352,-17.8217582590636));
#34968=CARTESIAN_POINT('Origin',(38.5,59.4602420414948,-20.1546860901778));
#34969=CARTESIAN_POINT('Origin',(38.5,49.4619799081484,-8.97279205057551));
#34970=CARTESIAN_POINT('Origin',(38.5,59.4602420414948,-20.1546860901778));
#34971=CARTESIAN_POINT('Origin',(38.5,52.3038298561492,-26.5535738555194));
#34972=CARTESIAN_POINT('',(38.5,49.6947212469087,-28.8865016866336));
#34973=CARTESIAN_POINT('Origin',(38.5,52.3038298561492,-26.5535738555194));
#34974=CARTESIAN_POINT('',(38.5,49.6947212469087,-28.8865016866336));
#34975=CARTESIAN_POINT('Origin',(39.7,49.6947212469087,-28.8865016866336));
#34976=CARTESIAN_POINT('',(39.7,49.6947212469087,-28.8865016866336));
#34977=CARTESIAN_POINT('',(39.7,49.6947212469087,-28.8865016866336));
#34978=CARTESIAN_POINT('',(39.7,49.6947212469087,-28.8865016866336));
#34979=CARTESIAN_POINT('Origin',(39.7,48.9492616442685,-29.5530524955233));
#34980=CARTESIAN_POINT('',(39.7,48.9492616442685,-29.5530524955233));
#34981=CARTESIAN_POINT('',(39.7,48.9492616442685,-29.5530524955233));
#34982=CARTESIAN_POINT('',(39.7,38.9509995109222,-18.3711584559211));
#34983=CARTESIAN_POINT('',(39.7,48.9492616442685,-29.5530524955233));
#34984=CARTESIAN_POINT('',(39.7,38.9509995109222,-18.3711584559211));
#34985=CARTESIAN_POINT('Origin',(40.5,48.9492616442685,-29.5530524955233));
#34986=CARTESIAN_POINT('',(40.5,38.9509995109222,-18.3711584559211));
#34987=CARTESIAN_POINT('',(40.5,38.9509995109222,-18.3711584559211));
#34988=CARTESIAN_POINT('',(40.5,48.9492616442685,-29.5530524955233));
#34989=CARTESIAN_POINT('',(40.5,48.9492616442685,-29.5530524955233));
#34990=CARTESIAN_POINT('',(40.5,48.9492616442685,-29.5530524955233));
#34991=CARTESIAN_POINT('Origin',(40.5,48.9492616442685,-29.5530524955233));
#34992=CARTESIAN_POINT('',(40.5,38.9509995109222,-18.3711584559211));
#34993=CARTESIAN_POINT('',(40.5,49.6947212469087,-28.8865016866336));
#34994=CARTESIAN_POINT('',(40.5,48.9492616442685,-29.5530524955233));
#34995=CARTESIAN_POINT('',(40.5,49.6947212469087,-28.8865016866336));
#34996=CARTESIAN_POINT('Origin',(40.5,49.6947212469087,-28.8865016866336));
#34997=CARTESIAN_POINT('',(48.2499021086877,41.0302398188277,-16.5120110196252));
#34998=CARTESIAN_POINT('',(48.2499021086877,51.028501952174,-27.6939050592275));
#34999=CARTESIAN_POINT('',(40.5,39.6964591135624,-17.7046076470313));
#35000=CARTESIAN_POINT('',(40.5,49.6947212469087,-28.8865016866336));
#35001=CARTESIAN_POINT('Origin',(38.5,49.4619799081484,-8.97279205057551));
#35002=CARTESIAN_POINT('',(48.8,48.8656122260362,-9.50603269768731));
#35003=CARTESIAN_POINT('',(48.8,42.901935404915,-14.8384391688054));
#35004=CARTESIAN_POINT('',(49.8,49.284600769485,-9.13139515654859));
#35005=CARTESIAN_POINT('',(49.8,42.4829468614662,-15.213076709944));
#35006=CARTESIAN_POINT('',(48.2499021086877,50.7373078121236,-7.83246084686749));
#35007=CARTESIAN_POINT('Origin',(47.8,49.284600769485,-9.13139515654859));
#35008=CARTESIAN_POINT('',(40.5,52.0710885173889,-6.63986421946138));
#35009=CARTESIAN_POINT('',(48.,49.4619799081484,-8.97279205057552));
#35010=CARTESIAN_POINT('',(45.4,49.4619799081483,-8.97279205057553));
#35011=CARTESIAN_POINT('Origin',(48.,48.8656122260362,-9.50603269768731));
#35012=CARTESIAN_POINT('Origin',(47.8,52.4812089948126,-26.3949707495463));
#35013=CARTESIAN_POINT('',(49.8,42.4829468614662,-15.213076709944));
#35014=CARTESIAN_POINT('',(49.8,52.4812089948126,-26.3949707495463));
#35015=CARTESIAN_POINT('Origin',(47.8,42.4829468614662,-15.213076709944));
#35016=CARTESIAN_POINT('Origin',(47.8,59.2828629028313,-20.3132891961508));
#35017=CARTESIAN_POINT('',(48.2499021086877,57.2541837104536,-15.1208290445089));
#35018=CARTESIAN_POINT('Origin',(47.7999999998822,56.4976327370815,-17.198332999803));
#35019=CARTESIAN_POINT('',(48.2499021086877,60.7355699454699,-19.0143548864697));
#35020=CARTESIAN_POINT('',(49.8,59.2828629028313,-20.3132891961508));
#35021=CARTESIAN_POINT('Origin',(38.5,49.4619799081484,-8.97279205057551));
#35022=CARTESIAN_POINT('Origin',(38.5,49.4619799081484,-8.97279205057551));
#35023=CARTESIAN_POINT('',(49.8,42.4829468614662,-15.213076709944));
#35024=CARTESIAN_POINT('',(48.8,42.901935404915,-14.8384391688054));
#35025=CARTESIAN_POINT('',(48.8,42.901935404915,-14.8384391688054));
#35026=CARTESIAN_POINT('',(48.,42.3055677228029,-15.3716798159172));
#35027=CARTESIAN_POINT('Origin',(48.,42.901935404915,-14.8384391688054));
#35028=CARTESIAN_POINT('',(45.4,42.3055677228029,-15.3716798159172));
#35029=CARTESIAN_POINT('Origin',(40.5,62.0693506507352,-17.8217582590636));
#35030=CARTESIAN_POINT('',(46.,61.1227846456323,-18.6681278465427));
#35031=CARTESIAN_POINT('',(45.1007678884438,62.6689719994181,-20.0858984152072));
#35032=CARTESIAN_POINT('',(40.5,62.0693506507352,-17.8217582590636));
#35033=CARTESIAN_POINT('Origin',(38.5,59.4602420414948,-20.1546860901778));
#35034=CARTESIAN_POINT('',(46.,59.4602420414948,-20.1546860901778));
#35035=CARTESIAN_POINT('',(46.,65.7609714429338,-14.5209049110894));
#35036=CARTESIAN_POINT('',(45.4,59.4602420414948,-20.1546860901778));
#35037=CARTESIAN_POINT('',(45.4,59.4602420414948,-20.1546860901778));
#35038=CARTESIAN_POINT('',(45.4,52.3038298561492,-26.5535738555194));
#35039=CARTESIAN_POINT('',(45.4,59.4602420414948,-20.1546860901778));
#35040=CARTESIAN_POINT('',(45.4,52.3038298561492,-26.5535738555194));
#35041=CARTESIAN_POINT('Origin',(49.8,52.4812089948126,-26.3949707495463));
#35042=CARTESIAN_POINT('Origin',(46.,53.1054137160521,-5.71502497212683));
#35043=CARTESIAN_POINT('Origin',(48.8,42.901935404915,-14.8384391688054));
#35044=CARTESIAN_POINT('',(48.8,48.8656122260362,-9.50603269768731));
#35045=CARTESIAN_POINT('Origin',(48.,48.8656122260362,-9.50603269768731));
#35046=CARTESIAN_POINT('',(48.,56.3655418573637,-16.6936236493485));
#35047=CARTESIAN_POINT('',(48.,49.4619799081484,-8.97279205057552));
#35048=CARTESIAN_POINT('Origin',(48.0000000000003,55.7691741752514,-17.2268642964596));
#35049=CARTESIAN_POINT('Origin',(48.,42.901935404915,-14.8384391688054));
#35050=CARTESIAN_POINT('',(48.8,42.901935404915,-14.8384391688054));
#35051=CARTESIAN_POINT('',(48.,42.3055677228029,-15.3716798159172));
#35052=CARTESIAN_POINT('Origin',(45.4,42.3055677228029,-15.3716798159172));
#35053=CARTESIAN_POINT('',(45.4,42.3055677228029,-15.3716798159172));
#35054=CARTESIAN_POINT('',(45.4,42.3055677228029,-15.3716798159172));
#35055=CARTESIAN_POINT('',(45.4,42.3055677228029,-15.3716798159172));
#35056=CARTESIAN_POINT('Origin',(38.5,49.4619799081484,-8.97279205057551));
#35057=CARTESIAN_POINT('Origin',(45.4,49.4619799081483,-8.97279205057553));
#35058=CARTESIAN_POINT('',(51.3562786983429,51.1722037044851,-10.8854785774534));
#35059=CARTESIAN_POINT('',(45.4,49.4619799081483,-8.97279205057553));
#35060=CARTESIAN_POINT('',(45.4,49.4619799081483,-8.97279205057553));
#35061=CARTESIAN_POINT('',(45.4,49.4619799081483,-8.97279205057553));
#35062=CARTESIAN_POINT('Origin',(48.,48.8656122260362,-9.50603269768731));
#35063=CARTESIAN_POINT('',(45.4,49.4619799081483,-8.97279205057553));
#35064=CARTESIAN_POINT('Origin',(45.4,49.4619799081483,-8.97279205057553));
#35065=CARTESIAN_POINT('Origin',(42.5,51.3256289147487,-7.3064150283511));
#35066=CARTESIAN_POINT('',(38.5,51.3256289147488,-7.30641502835113));
#35067=CARTESIAN_POINT('',(38.5,51.3256289147488,-7.30641502835113));
#35068=CARTESIAN_POINT('',(42.5,51.3256289147488,-7.30641502835114));
#35069=CARTESIAN_POINT('',(42.5,51.3256289147488,-7.30641502835114));
#35070=CARTESIAN_POINT('',(42.5,51.3256289147487,-7.3064150283511));
#35071=CARTESIAN_POINT('Origin',(42.5,49.4619799081484,-8.97279205057552));
#35072=CARTESIAN_POINT('',(45.,49.4619799081483,-8.97279205057549));
#35073=CARTESIAN_POINT('',(45.,49.4619799081483,-8.97279205057549));
#35074=CARTESIAN_POINT('Origin',(42.5,49.4619799081484,-8.97279205057552));
#35075=CARTESIAN_POINT('Origin',(45.,49.4619799081483,-8.97279205057549));
#35076=CARTESIAN_POINT('',(45.,42.3055677228029,-15.3716798159172));
#35077=CARTESIAN_POINT('',(45.,42.3055677228029,-15.3716798159172));
#35078=CARTESIAN_POINT('',(45.,49.4619799081483,-8.97279205057549));
#35079=CARTESIAN_POINT('Origin',(42.5,42.3055677228029,-15.3716798159172));
#35080=CARTESIAN_POINT('',(42.5,40.4419187162025,-17.0380568381416));
#35081=CARTESIAN_POINT('',(42.5,40.4419187162025,-17.0380568381416));
#35082=CARTESIAN_POINT('Origin',(42.5,42.3055677228029,-15.3716798159172));
#35083=CARTESIAN_POINT('Origin',(42.5,40.4419187162025,-17.0380568381416));
#35084=CARTESIAN_POINT('',(38.5,40.4419187162025,-17.0380568381416));
#35085=CARTESIAN_POINT('',(38.5,40.4419187162025,-17.0380568381416));
#35086=CARTESIAN_POINT('',(42.5,40.4419187162025,-17.0380568381416));
#35087=CARTESIAN_POINT('Origin',(38.5,42.3055677228029,-15.3716798159172));
#35088=CARTESIAN_POINT('',(36.,42.3055677228029,-15.3716798159172));
#35089=CARTESIAN_POINT('',(36.,42.3055677228029,-15.3716798159172));
#35090=CARTESIAN_POINT('Origin',(38.5,42.3055677228029,-15.3716798159172));
#35091=CARTESIAN_POINT('Origin',(38.5,49.4619799081484,-8.9727920505755));
#35092=CARTESIAN_POINT('',(36.,49.4619799081484,-8.97279205057551));
#35093=CARTESIAN_POINT('',(36.,49.4619799081484,-8.97279205057551));
#35094=CARTESIAN_POINT('Origin',(38.5,49.4619799081484,-8.9727920505755));
#35095=CARTESIAN_POINT('Origin',(46.,65.7609714429338,-14.5209049110894));
#35096=CARTESIAN_POINT('Origin',(48.8,42.901935404915,-14.8384391688054));
#35097=CARTESIAN_POINT('Origin',(36.,49.4619799081484,-8.97279205057551));
#35098=CARTESIAN_POINT('',(36.,49.4619799081484,-8.97279205057551));
#35099=CARTESIAN_POINT('',(36.,49.4619799081484,-8.97279205057551));
#35100=CARTESIAN_POINT('',(36.,49.4619799081484,-8.97279205057551));
#35101=CARTESIAN_POINT('Origin',(40.35,54.8229336924257,-17.5938519925341));
#35102=CARTESIAN_POINT('',(40.35,54.8229336924257,-17.5938519925341));
#35103=CARTESIAN_POINT('',(40.35,48.1574256035281,-10.1392559661326));
#35104=CARTESIAN_POINT('Origin',(28.,52.5492819043732,-19.6268319596478));
#35105=CARTESIAN_POINT('Origin',(40.65,52.1020061427891,-20.0267624449817));
#35106=CARTESIAN_POINT('',(40.35,51.3872947315215,-19.2274408065706));
#35107=CARTESIAN_POINT('',(40.35,45.4364980538915,-12.5721664185802));
#35108=CARTESIAN_POINT('',(40.35,52.1020061427891,-20.0267624449817));
#35109=CARTESIAN_POINT('',(40.65,51.3872947315215,-19.2274408065706));
#35110=CARTESIAN_POINT('',(40.65,51.3872947315215,-19.2274408065706));
#35111=CARTESIAN_POINT('',(40.65,45.4364980538915,-12.5721664185802));
#35112=CARTESIAN_POINT('',(40.65,52.1020061427891,-20.0267624449817));
#35113=CARTESIAN_POINT('',(40.65,45.4364980538915,-12.5721664185802));
#35114=CARTESIAN_POINT('Origin',(40.35,52.9965576659573,-19.2269014743139));
#35115=CARTESIAN_POINT('',(40.65,52.2818462546897,-18.4275798359029));
#35116=CARTESIAN_POINT('',(40.65,46.3310495770598,-11.7723054479125));
#35117=CARTESIAN_POINT('',(40.65,52.9965576659573,-19.2269014743139));
#35118=CARTESIAN_POINT('',(40.35,52.2818462546897,-18.4275798359029));
#35119=CARTESIAN_POINT('',(40.35,52.2818462546897,-18.4275798359029));
#35120=CARTESIAN_POINT('',(40.35,46.3310495770598,-11.7723054479125));
#35121=CARTESIAN_POINT('',(40.35,52.9965576659573,-19.2269014743139));
#35122=CARTESIAN_POINT('',(40.35,46.3310495770598,-11.7723054479125));
#35123=CARTESIAN_POINT('Origin',(40.65,52.9965576659573,-19.2269014743139));
#35124=CARTESIAN_POINT('',(40.65,52.6238278646372,-19.5601768787589));
#35125=CARTESIAN_POINT('',(40.65,52.4747359441092,-19.6934870405368));
#35126=CARTESIAN_POINT('',(40.65,52.9965576659573,-19.2269014743139));
#35127=CARTESIAN_POINT('',(40.65,52.6238278646372,-19.5601768787589));
#35128=CARTESIAN_POINT('',(40.65,46.3310495770598,-11.7723054479125));
#35129=CARTESIAN_POINT('',(40.65,52.4747359441092,-19.6934870405368));
#35130=CARTESIAN_POINT('Origin',(28.,52.6238278646372,-19.5601768787589));
#35131=CARTESIAN_POINT('',(40.35,52.6238278646372,-19.5601768787589));
#35132=CARTESIAN_POINT('',(40.35,52.6238278646372,-19.5601768787589));
#35133=CARTESIAN_POINT('',(40.65,52.6238278646372,-19.5601768787589));
#35134=CARTESIAN_POINT('Origin',(28.,52.5492819043732,-19.6268319596478));
#35135=CARTESIAN_POINT('',(40.35,52.4747359441092,-19.6934870405368));
#35136=CARTESIAN_POINT('',(40.35,52.1020061427891,-20.0267624449817));
#35137=CARTESIAN_POINT('',(40.35,52.4747359441092,-19.6934870405368));
#35138=CARTESIAN_POINT('Origin',(40.35,52.1020061427891,-20.0267624449817));
#35139=CARTESIAN_POINT('',(40.35,52.4747359441092,-19.6934870405368));
#35140=CARTESIAN_POINT('',(40.35,45.4364980538915,-12.5721664185802));
#35141=CARTESIAN_POINT('Origin',(40.35,50.2756301163208,-21.6598119267616));
#35142=CARTESIAN_POINT('',(40.65,43.6101220274232,-14.2052159003601));
#35143=CARTESIAN_POINT('',(40.65,50.2756301163208,-21.6598119267616));
#35144=CARTESIAN_POINT('',(40.35,43.6101220274232,-14.2052159003601));
#35145=CARTESIAN_POINT('Origin',(40.65,50.2756301163208,-21.6598119267616));
#35146=CARTESIAN_POINT('',(40.65,43.6101220274232,-14.2052159003601));
#35147=CARTESIAN_POINT('Origin',(28.,52.4747359441092,-19.6934870405368));
#35148=CARTESIAN_POINT('Origin',(42.5,49.4619799081484,-8.97279205057552));
#62951=UNCERTAINTY_MEASURE_WITH_UNIT(LENGTH_MEASURE(0.01),#62975,
'DISTANCE_ACCURACY_VALUE',
'Maximum model space distance between geometric entities at asserted c
onnectivities');
#62960=UNCERTAINTY_MEASURE_WITH_UNIT(LENGTH_MEASURE(0.01),#62975,
'DISTANCE_ACCURACY_VALUE',
'Maximum model space distance between geometric entities at asserted c
onnectivities');
#62965=(
GEOMETRIC_REPRESENTATION_CONTEXT(3)
GLOBAL_UNCERTAINTY_ASSIGNED_CONTEXT((#62951))
GLOBAL_UNIT_ASSIGNED_CONTEXT((#62975,#62977,#62978))
REPRESENTATION_CONTEXT('','3D')
);
#62974=(
GEOMETRIC_REPRESENTATION_CONTEXT(3)
GLOBAL_UNCERTAINTY_ASSIGNED_CONTEXT((#62960))
GLOBAL_UNIT_ASSIGNED_CONTEXT((#62975,#62977,#62978))
REPRESENTATION_CONTEXT('','3D')
);
#62975=(
LENGTH_UNIT()
NAMED_UNIT(*)
SI_UNIT(.MILLI.,.METRE.)
);
#62977=(
NAMED_UNIT(*)
PLANE_ANGLE_UNIT()
SI_UNIT($,.RADIAN.)
);
#62978=(
NAMED_UNIT(*)
SI_UNIT($,.STERADIAN.)
SOLID_ANGLE_UNIT()
);
#62983=SHAPE_DEFINITION_REPRESENTATION(#62996,#63024);
#62996=PRODUCT_DEFINITION_SHAPE('',$,#63038);
#63024=SHAPE_REPRESENTATION('',(#15679),#62965);
#63033=PRODUCT_DEFINITION_CONTEXT('part definition',#63074,'design');
#63038=PRODUCT_DEFINITION('TPS - Throttle Position Sensor',
'TPS - Throttle Position Sensor',#63051,#63033);
#63051=PRODUCT_DEFINITION_FORMATION('',$,#63080);
#63074=APPLICATION_CONTEXT(
'Core Data for Automotive Mechanical Design Process');
#63075=PRODUCT_CONTEXT('part definition',#63074,'mechanical');
#63080=PRODUCT('TPS - Throttle Position Sensor',
'TPS - Throttle Position Sensor',$,(#63075));
#63090=PRESENTATION_STYLE_ASSIGNMENT((#63092));
#63092=SURFACE_STYLE_USAGE(.BOTH.,#63094);
#63094=SURFACE_SIDE_STYLE('',(#63096));
#63096=SURFACE_STYLE_FILL_AREA(#63098);
#63098=FILL_AREA_STYLE('Opaque(202,209,238)',(#63100));
#63100=FILL_AREA_STYLE_COLOUR('Opaque(202,209,238)',#63102);
#63102=COLOUR_RGB('Opaque(202,209,238)', 0.66274510, 0.83137255, 0.94901961);
ENDSEC;
END-ISO-10303-21;
